ISO-10303-21;
HEADER;
FILE_DESCRIPTION (('STEP AP214'),
    '1' );
FILE_NAME ('Top Cover.step',
    '2026-10-24T11:32:06',
    ( '' ),
    ( '' ),
    'SwSTEP 2.0',
    'SolidWorks 2025',
    '' );
FILE_SCHEMA (( 'AUTOMOTIVE_DESIGN' ));
ENDSEC;

DATA;
#7=EDGE_CURVE ( 'NONE', #12139, #21915, #4265, .T. ) ;
#64=ORIENTED_EDGE ( 'NONE', *, *, #33322, .T. ) ;
#131=FACE_OUTER_BOUND ( 'NONE', #28949, .T. ) ;
#191=DIRECTION ( 'NONE',  ( 1.000000000000000000, 0.000000000000000000, -0.000000000000000000 ) ) ;
#270=LINE ( 'NONE', #11643, #31070 ) ;
#311=ORIENTED_EDGE ( 'NONE', *, *, #28876, .T. ) ;
#333=ORIENTED_EDGE ( 'NONE', *, *, #14896, .T. ) ;
#343=ORIENTED_EDGE ( 'NONE', *, *, #20618, .T. ) ;
#378=DIRECTION ( 'NONE',  ( 0.000000000000000000, -1.000000000000000000, 0.000000000000000000 ) ) ;
#479=VECTOR ( 'NONE', #29669, 39.37007874015748143 ) ;
#513=DIRECTION ( 'NONE',  ( 0.000000000000000000, -1.000000000000000000, 0.000000000000000000 ) ) ;
#565=ORIENTED_EDGE ( 'NONE', *, *, #39222, .T. ) ;
#638=FACE_OUTER_BOUND ( 'NONE', #44764, .T. ) ;
#676=DIRECTION ( 'NONE',  ( -0.7071067811865481278, 0.7071067811865469066, 4.592716591420704405E-16 ) ) ;
#692=ORIENTED_EDGE ( 'NONE', *, *, #46921, .F. ) ;
#699=VECTOR ( 'NONE', #17087, 39.37007874015748143 ) ;
#758=CARTESIAN_POINT ( 'NONE',  ( 1.181102362204724532, 0.4724409448818893686, 1.181102362204724088 ) ) ;
#805=LINE ( 'NONE', #8805, #22763 ) ;
#854=EDGE_CURVE ( 'NONE', #21915, #35502, #15750, .T. ) ;
#922=UNCERTAINTY_MEASURE_WITH_UNIT (LENGTH_MEASURE( 1.000000000000000082E-05 ), #37201, 'distance_accuracy_value', 'NONE');
#943=LINE ( 'NONE', #39931, #45738 ) ;
#950=VECTOR ( 'NONE', #42020, 39.37007874015748143 ) ;
#1027=DIRECTION ( 'NONE',  ( -8.653332088726061579E-16, 0.7071067811865483499, -0.7071067811865466846 ) ) ;
#1052=LINE ( 'NONE', #16811, #39981 ) ;
#1076=EDGE_CURVE ( 'NONE', #17210, #50226, #17802, .T. ) ;
#1189=CARTESIAN_POINT ( 'NONE',  ( 1.122047244094487750, 0.5314960629921257063, -1.062992125984252079 ) ) ;
#1200=CARTESIAN_POINT ( 'NONE',  ( -1.062992125984252079, 0.4235180831842794702, -1.014069264286642236 ) ) ;
#1391=ADVANCED_FACE ( 'NONE', ( #27818 ), #12339, .T. ) ;
#1501=ADVANCED_FACE ( 'NONE', ( #30321 ), #9943, .F. ) ;
#1541=ORIENTED_EDGE ( 'NONE', *, *, #43831, .T. ) ;
#1645=CARTESIAN_POINT ( 'NONE',  ( -1.181102362204724310, 0.4724409448818890911, -1.062992125984252079 ) ) ;
#1686=DIRECTION ( 'NONE',  ( 1.156482317317871478E-16, 0.000000000000000000, 1.000000000000000000 ) ) ;
#1743=FACE_OUTER_BOUND ( 'NONE', #34807, .T. ) ;
#1839=LINE ( 'NONE', #17592, #699 ) ;
#1852=ORIENTED_EDGE ( 'NONE', *, *, #39006, .T. ) ;
#1937=ORIENTED_EDGE ( 'NONE', *, *, #20104, .F. ) ;
#2004=PLANE ( 'NONE',  #47446 ) ;
#2075=VERTEX_POINT ( 'NONE', #31888 ) ;
#2130=ORIENTED_EDGE ( 'NONE', *, *, #10354, .T. ) ;
#2169=ORIENTED_EDGE ( 'NONE', *, *, #14575, .T. ) ;
#2222=ORIENTED_EDGE ( 'NONE', *, *, #33322, .F. ) ;
#2232=CARTESIAN_POINT ( 'NONE',  ( 1.181102362204724310, 0.5905511811023621549, -1.062992125984252079 ) ) ;
#2245=EDGE_CURVE ( 'NONE', #2075, #30992, #24382, .T. ) ;
#2417=EDGE_CURVE ( 'NONE', #31066, #3209, #15553, .T. ) ;
#2527=ORIENTED_EDGE ( 'NONE', *, *, #41949, .F. ) ;
#2544=PLANE ( 'NONE',  #32716 ) ;
#2578=CARTESIAN_POINT ( 'NONE',  ( 1.062992125984252079, 0.000000000000000000, 1.014069264286641570 ) ) ;
#2584=DIRECTION ( 'NONE',  ( -5.782411586589357392E-17, -0.000000000000000000, -1.000000000000000000 ) ) ;
#2659=DIRECTION ( 'NONE',  ( -5.782411586589357392E-17, 0.000000000000000000, -1.000000000000000000 ) ) ;
#2708=FACE_OUTER_BOUND ( 'NONE', #33108, .T. ) ;
#2739=VECTOR ( 'NONE', #27011, 39.37007874015748143 ) ;
#2799=ORIENTED_EDGE ( 'NONE', *, *, #13198, .F. ) ;
#2832=CARTESIAN_POINT ( 'NONE',  ( -1.181102362204724088, 0.5905511811023621549, 1.062992125984251635 ) ) ;
#2887=( NAMED_UNIT ( * ) PLANE_ANGLE_UNIT ( ) SI_UNIT ( $, .RADIAN. ) );
#2930=ORIENTED_EDGE ( 'NONE', *, *, #43107, .T. ) ;
#3048=DIRECTION ( 'NONE',  ( 0.000000000000000000, 1.000000000000000000, 0.000000000000000000 ) ) ;
#3209=VERTEX_POINT ( 'NONE', #42225 ) ;
#3258=CARTESIAN_POINT ( 'NONE',  ( -1.051609096396380005, 0.4349011127721510994, 1.025452293874513199 ) ) ;
#3305=LINE ( 'NONE', #19047, #479 ) ;
#3358=EDGE_CURVE ( 'NONE', #21585, #25120, #31376, .T. ) ;
#3362=CARTESIAN_POINT ( 'NONE',  ( -1.097585813245683273, 0.000000000000000000, -0.9794755770252108196 ) ) ;
#3386=ORIENTED_EDGE ( 'NONE', *, *, #32466, .F. ) ;
#3387=CARTESIAN_POINT ( 'NONE',  ( -1.181102362204724310, 0.4724409448818890911, -1.062992125984252079 ) ) ;
#3584=DIRECTION ( 'NONE',  ( -0.5773502691896253980, 0.5773502691896246208, 0.5773502691896272854 ) ) ;
#3589=LINE ( 'NONE', #30959, #17324 ) ;
#3594=DIRECTION ( 'NONE',  ( -0.000000000000000000, 1.000000000000000000, -0.000000000000000000 ) ) ;
#3627=LINE ( 'NONE', #50805, #21570 ) ;
#3726=AXIS2_PLACEMENT_3D ( 'NONE', #24646, #40900, #378 ) ;
#3737=DIRECTION ( 'NONE',  ( 0.7071067811865466846, 0.000000000000000000, 0.7071067811865483499 ) ) ;
#3781=LINE ( 'NONE', #50958, #30181 ) ;
#3821=AXIS2_PLACEMENT_3D ( 'NONE', #10400, #46736, #26143 ) ;
#3834=LINE ( 'NONE', #27310, #28126 ) ;
#3860=DIRECTION ( 'NONE',  ( 1.000000000000000000, 0.000000000000000000, 0.000000000000000000 ) ) ;
#3864=VECTOR ( 'NONE', #13498, 39.37007874015748143 ) ;
#4037=PLANE ( 'NONE',  #37634 ) ;
#4058=CARTESIAN_POINT ( 'NONE',  ( -1.062992125984251635, 0.5905511811023621549, -1.062992125984252079 ) ) ;
#4068=FACE_OUTER_BOUND ( 'NONE', #17287, .T. ) ;
#4138=PLANE ( 'NONE',  #32254 ) ;
#4148=DIRECTION ( 'NONE',  ( -0.5773502691896259531, 0.5773502691896245098, -0.5773502691896270633 ) ) ;
#4181=DIRECTION ( 'NONE',  ( 0.000000000000000000, 1.000000000000000000, 0.000000000000000000 ) ) ;
#4189=VERTEX_POINT ( 'NONE', #25029 ) ;
#4207=CARTESIAN_POINT ( 'NONE',  ( -1.025452293874513199, 0.4349011127721511549, 1.051609096396380005 ) ) ;
#4231=DIRECTION ( 'NONE',  ( -0.5773502691896265082, 0.5773502691896255090, -0.5773502691896251759 ) ) ;
#4265=LINE ( 'NONE', #39634, #8954 ) ;
#4273=LINE ( 'NONE', #35264, #38949 ) ;
#4287=EDGE_CURVE ( 'NONE', #48480, #42546, #5668, .T. ) ;
#4328=EDGE_CURVE ( 'NONE', #3209, #26202, #6434, .T. ) ;
#4346=VECTOR ( 'NONE', #18651, 39.37007874015748143 ) ;
#4375=ORIENTED_EDGE ( 'NONE', *, *, #18637, .T. ) ;
#4399=PRODUCT_CONTEXT ( 'NONE', #9120, 'mechanical' ) ;
#4473=EDGE_CURVE ( 'NONE', #30518, #49043, #35765, .T. ) ;
#4491=LINE ( 'NONE', #16628, #24045 ) ;
#4492=VECTOR ( 'NONE', #26532, 39.37007874015748854 ) ;
#4612=LINE ( 'NONE', #24492, #38981 ) ;
#4620=CARTESIAN_POINT ( 'NONE',  ( -1.014069264286641570, 0.4724409448818898127, 1.014069264286641570 ) ) ;
#4651=CARTESIAN_POINT ( 'NONE',  ( 1.062992125984251413, 0.5905511811023621549, 1.062992125984251413 ) ) ;
#4657=VERTEX_POINT ( 'NONE', #14056 ) ;
#4771=DIRECTION ( 'NONE',  ( 0.5773502691896268413, -0.5773502691896258421, -0.5773502691896243988 ) ) ;
#4781=DIRECTION ( 'NONE',  ( 0.000000000000000000, 0.7071067811865466846, -0.7071067811865483499 ) ) ;
#4820=DIRECTION ( 'NONE',  ( 0.000000000000000000, -1.000000000000000000, 0.000000000000000000 ) ) ;
#4858=ORIENTED_EDGE ( 'NONE', *, *, #29604, .F. ) ;
#4881=DIRECTION ( 'NONE',  ( 1.000000000000000000, 0.000000000000000000, -1.156482317317871478E-16 ) ) ;
#4934=DIRECTION ( 'NONE',  ( 0.000000000000000000, 0.000000000000000000, -1.000000000000000000 ) ) ;
#4980=FACE_OUTER_BOUND ( 'NONE', #10040, .T. ) ;
#4984=LINE ( 'NONE', #24608, #41176 ) ;
#5020=SHAPE_REPRESENTATION ( 'Top Cover', ( #26741 ), #16013 ) ;
#5042=DIRECTION ( 'NONE',  ( 5.782411586589357392E-17, 0.000000000000000000, 1.000000000000000000 ) ) ;
#5081=DIRECTION ( 'NONE',  ( 0.7071067811865486830, 0.000000000000000000, 0.7071067811865462405 ) ) ;
#5108=VERTEX_POINT ( 'NONE', #16597 ) ;
#5247=EDGE_LOOP ( 'NONE', ( #565, #311, #9454, #26075, #14028, #42552 ) ) ;
#5272=PLANE ( 'NONE',  #3726 ) ;
#5320=CARTESIAN_POINT ( 'NONE',  ( -1.181102362204724088, 0.000000000000000000, 1.062992125984251413 ) ) ;
#5357=ORIENTED_EDGE ( 'NONE', *, *, #47014, .T. ) ;
#5367=DIRECTION ( 'NONE',  ( 0.000000000000000000, -0.000000000000000000, 1.000000000000000000 ) ) ;
#5382=DIRECTION ( 'NONE',  ( -1.156482317317871478E-16, 0.000000000000000000, -1.000000000000000000 ) ) ;
#5420=VECTOR ( 'NONE', #40593, 39.37007874015748143 ) ;
#5511=EDGE_CURVE ( 'NONE', #3209, #45101, #10280, .T. ) ;
#5668=LINE ( 'NONE', #35880, #40388 ) ;
#5748=CARTESIAN_POINT ( 'NONE',  ( 1.181102362204724310, 0.000000000000000000, -1.062992125984252079 ) ) ;
#5846=DIRECTION ( 'NONE',  ( 1.442222014787672788E-15, -0.7071067811865483499, -0.7071067811865465735 ) ) ;
#5855=VECTOR ( 'NONE', #11843, 39.37007874015748143 ) ;
#5882=CARTESIAN_POINT ( 'NONE',  ( -1.051609096396380449, 0.4349011127721510994, -1.025452293874513643 ) ) ;
#5898=EDGE_CURVE ( 'NONE', #49043, #48480, #47523, .T. ) ;
#5924=CARTESIAN_POINT ( 'NONE',  ( 1.038530695135447157, 0.4349011127721510994, 1.038530695135446491 ) ) ;
#6385=EDGE_CURVE ( 'NONE', #4189, #47727, #16464, .T. ) ;
#6404=CARTESIAN_POINT ( 'NONE',  ( -1.030376884852511887, 0.4561333243160197171, -1.046684505418382205 ) ) ;
#6434=LINE ( 'NONE', #33304, #10714 ) ;
#6496=ORIENTED_EDGE ( 'NONE', *, *, #36635, .T. ) ;
#6538=DIRECTION ( 'NONE',  ( -0.5773502691896265082, 0.5773502691896255090, 0.5773502691896251759 ) ) ;
#6587=LINE ( 'NONE', #27197, #20335 ) ;
#6589=PRODUCT_DEFINITION_CONTEXT ( 'detailed design', #17053, 'design' ) ;
#6625=DIRECTION ( 'NONE',  ( 0.5773502691896260641, 0.5773502691896273964, 0.5773502691896240657 ) ) ;
#6682=ORIENTED_EDGE ( 'NONE', *, *, #21479, .F. ) ;
#6705=VECTOR ( 'NONE', #43010, 39.37007874015748143 ) ;
#6706=PLANE ( 'NONE',  #24179 ) ;
#6721=ORIENTED_EDGE ( 'NONE', *, *, #26758, .F. ) ;
#6829=CARTESIAN_POINT ( 'NONE',  ( 0.9794755770252100424, 0.5070346321433213399, -1.025452293874514087 ) ) ;
#6952=CARTESIAN_POINT ( 'NONE',  ( 1.062992125984251413, 0.5905511811023621549, -1.181102362204724754 ) ) ;
#6974=AXIS2_PLACEMENT_3D ( 'NONE', #12622, #4881, #13650 ) ;
#7032=CARTESIAN_POINT ( 'NONE',  ( 0.000000000000000000, 0.5070346321433212289, 0.9794755770252101534 ) ) ;
#7036=LINE ( 'NONE', #21945, #43011 ) ;
#7083=CARTESIAN_POINT ( 'NONE',  ( 1.181102362204724310, 0.4724409448818890911, -1.181102362204724754 ) ) ;
#7091=PRODUCT_DEFINITION_SHAPE ( 'NONE', 'NONE',  #16821 ) ;
#7123=ORIENTED_EDGE ( 'NONE', *, *, #15259, .T. ) ;
#7176=CARTESIAN_POINT ( 'NONE',  ( 1.062992125984251413, 0.4724409448818890911, -1.181102362204724754 ) ) ;
#7226=CARTESIAN_POINT ( 'NONE',  ( -1.062992125984251635, 0.5905511811023621549, 1.014069264286641570 ) ) ;
#7253=VERTEX_POINT ( 'NONE', #21487 ) ;
#7457=CARTESIAN_POINT ( 'NONE',  ( -0.9948011493083110945, 0.4042499682059492172, 1.112911385528783992 ) ) ;
#7604=VERTEX_POINT ( 'NONE', #33062 ) ;
#7793=DIRECTION ( 'NONE',  ( -0.000000000000000000, 1.000000000000000000, -0.000000000000000000 ) ) ;
#7800=CARTESIAN_POINT ( 'NONE',  ( 1.062992125984251635, 0.5905511811023621549, 1.181102362204724088 ) ) ;
#7824=EDGE_CURVE ( 'NONE', #4657, #23441, #39194, .T. ) ;
#7827=EDGE_CURVE ( 'NONE', #47028, #20197, #3834, .T. ) ;
#7940=DIRECTION ( 'NONE',  ( 0.000000000000000000, 0.000000000000000000, 1.000000000000000000 ) ) ;
#7960=CARTESIAN_POINT ( 'NONE',  ( -1.181102362204724310, 0.000000000000000000, -1.181102362204724754 ) ) ;
#8011=EDGE_LOOP ( 'NONE', ( #11681, #13362, #343, #40459 ) ) ;
#8039=ORIENTED_EDGE ( 'NONE', *, *, #25325, .T. ) ;
#8054=ORIENTED_EDGE ( 'NONE', *, *, #47562, .T. ) ;
#8055=EDGE_CURVE ( 'NONE', #4189, #25120, #25942, .T. ) ;
#8169=CARTESIAN_POINT ( 'NONE',  ( -1.062992125984251635, 0.4235180831842794702, 1.014069264286641570 ) ) ;
#8215=DIRECTION ( 'NONE',  ( 0.000000000000000000, -1.000000000000000000, 0.000000000000000000 ) ) ;
#8219=LINE ( 'NONE', #7960, #28664 ) ;
#8350=PRODUCT ( 'Top Cover', 'Top Cover', '', ( #4399 ) ) ;
#8441=VECTOR ( 'NONE', #5042, 39.37007874015748143 ) ;
#8522=CARTESIAN_POINT ( 'NONE',  ( 1.051609096396380449, 0.4349011127721511549, 1.025452293874513199 ) ) ;
#8556=VERTEX_POINT ( 'NONE', #5748 ) ;
#8580=CARTESIAN_POINT ( 'NONE',  ( -1.181102362204724310, 0.5905511811023621549, -1.062992125984252079 ) ) ;
#8628=CARTESIAN_POINT ( 'NONE',  ( -1.097585813245683273, 0.5905511811023621549, -0.9794755770252108196 ) ) ;
#8748=VERTEX_POINT ( 'NONE', #32818 ) ;
#8805=CARTESIAN_POINT ( 'NONE',  ( 0.6529837180168069910, 0.8335264911517238362, 0.6529837180168082122 ) ) ;
#8820=CARTESIAN_POINT ( 'NONE',  ( 1.062992125984252079, 0.000000000000000000, -1.014069264286642014 ) ) ;
#8873=VERTEX_POINT ( 'NONE', #14194 ) ;
#8907=DIRECTION ( 'NONE',  ( 1.000000000000000000, 0.000000000000000000, 0.000000000000000000 ) ) ;
#8918=VECTOR ( 'NONE', #26366, 39.37007874015748143 ) ;
#8944=CARTESIAN_POINT ( 'NONE',  ( -1.181102362204724088, 0.4724409448818890911, 1.062992125984251413 ) ) ;
#8954=VECTOR ( 'NONE', #19998, 39.37007874015748143 ) ;
#8956=PLANE ( 'NONE',  #50602 ) ;
#8979=ADVANCED_FACE ( 'NONE', ( #10581 ), #6706, .T. ) ;
#9115=ORIENTED_EDGE ( 'NONE', *, *, #5511, .F. ) ;
#9120=APPLICATION_CONTEXT ( 'automotive_design' ) ;
#9127=VECTOR ( 'NONE', #26206, 39.37007874015748143 ) ;
#9178=UNCERTAINTY_MEASURE_WITH_UNIT (LENGTH_MEASURE( 1.000000000000000082E-05 ), #50817, 'distance_accuracy_value', 'NONE');
#9189=CARTESIAN_POINT ( 'NONE',  ( 1.062992125984251413, 0.000000000000000000, -1.181102362204724754 ) ) ;
#9279=CARTESIAN_POINT ( 'NONE',  ( 1.181102362204724532, 0.4724409448818893686, 1.062992125984251413 ) ) ;
#9381=DIRECTION ( 'NONE',  ( 0.000000000000000000, 0.7071067811865466846, -0.7071067811865483499 ) ) ;
#9454=ORIENTED_EDGE ( 'NONE', *, *, #18983, .T. ) ;
#9461=ORIENTED_EDGE ( 'NONE', *, *, #46921, .T. ) ;
#9493=ORIENTED_EDGE ( 'NONE', *, *, #10354, .F. ) ;
#9563=DIRECTION ( 'NONE',  ( 0.000000000000000000, 0.000000000000000000, -1.000000000000000000 ) ) ;
#9575=PLANE ( 'NONE',  #29185 ) ;
#9715=ADVANCED_FACE ( 'NONE', ( #35236 ), #16118, .T. ) ;
#9731=ORIENTED_EDGE ( 'NONE', *, *, #39061, .F. ) ;
#9802=CARTESIAN_POINT ( 'NONE',  ( 1.025452293874513421, 0.5070346321433218950, 0.9794755770252094873 ) ) ;
#9943=PLANE ( 'NONE',  #32848 ) ;
#10032=DIRECTION ( 'NONE',  ( 5.782411586589357392E-17, -0.000000000000000000, 1.000000000000000000 ) ) ;
#10040=EDGE_LOOP ( 'NONE', ( #22797, #44448, #23767, #31087 ) ) ;
#10219=EDGE_LOOP ( 'NONE', ( #43289, #48736, #18251, #23921 ) ) ;
#10233=EDGE_LOOP ( 'NONE', ( #10393, #40763, #21471, #18060, #19632, #1852 ) ) ;
#10280=LINE ( 'NONE', #18541, #39647 ) ;
#10297=VERTEX_POINT ( 'NONE', #30161 ) ;
#10354=EDGE_CURVE ( 'NONE', #26402, #50880, #42536, .T. ) ;
#10393=ORIENTED_EDGE ( 'NONE', *, *, #35623, .T. ) ;
#10400=CARTESIAN_POINT ( 'NONE',  ( 1.181102362204724532, 0.5905511811023621549, 1.062992125984251413 ) ) ;
#10460=CARTESIAN_POINT ( 'NONE',  ( -1.181102362204724088, 0.000000000000000000, 1.181102362204724088 ) ) ;
#10461=ADVANCED_FACE ( 'NONE', ( #35811 ), #20313, .F. ) ;
#10473=EDGE_LOOP ( 'NONE', ( #29433, #2930, #31253, #23496 ) ) ;
#10524=ADVANCED_FACE ( 'NONE', ( #4068 ), #8956, .T. ) ;
#10538=DIRECTION ( 'NONE',  ( 0.7071067811865483499, 1.579007132194770110E-15, -0.7071067811865466846 ) ) ;
#10571=EDGE_LOOP ( 'NONE', ( #47866, #20010, #3386, #21874 ) ) ;
#10581=FACE_OUTER_BOUND ( 'NONE', #32876, .T. ) ;
#10612=CARTESIAN_POINT ( 'NONE',  ( 1.062992125984251413, 0.5905511811023621549, -1.181102362204724754 ) ) ;
#10674=LINE ( 'NONE', #46015, #34280 ) ;
#10704=CARTESIAN_POINT ( 'NONE',  ( 1.062992125984251413, 0.5905511811023621549, -1.062992125984252079 ) ) ;
#10714=VECTOR ( 'NONE', #37938, 39.37007874015748143 ) ;
#10838=CARTESIAN_POINT ( 'NONE',  ( -1.014069264286641570, 0.5905511811023621549, 1.062992125984251635 ) ) ;
#10945=CARTESIAN_POINT ( 'NONE',  ( -1.062992125984251413, 0.4724409448818890911, -1.181102362204724754 ) ) ;
#10960=CARTESIAN_POINT ( 'NONE',  ( 1.014069264286642014, 0.000000000000000000, 1.062992125984251635 ) ) ;
#11050=ORIENTED_EDGE ( 'NONE', *, *, #44486, .T. ) ;
#11056=AXIS2_PLACEMENT_3D ( 'NONE', #18283, #13909, #10032 ) ;
#11107=CARTESIAN_POINT ( 'NONE',  ( 1.062992125984252079, 0.5905511811023621549, -1.181102362204724754 ) ) ;
#11151=PLANE ( 'NONE',  #3821 ) ;
#11158=VECTOR ( 'NONE', #21846, 39.37007874015748143 ) ;
#11208=EDGE_CURVE ( 'NONE', #21585, #30221, #10674, .T. ) ;
#11225=DIRECTION ( 'NONE',  ( -1.000000000000000000, 0.000000000000000000, 0.000000000000000000 ) ) ;
#11262=ORIENTED_EDGE ( 'NONE', *, *, #23929, .T. ) ;
#11324=ORIENTED_EDGE ( 'NONE', *, *, #39841, .T. ) ;
#11325=ORIENTED_EDGE ( 'NONE', *, *, #17846, .F. ) ;
#11421=VECTOR ( 'NONE', #45346, 39.37007874015748143 ) ;
#11446=VECTOR ( 'NONE', #4771, 39.37007874015748854 ) ;
#11526=VECTOR ( 'NONE', #37511, 39.37007874015748143 ) ;
#11535=CARTESIAN_POINT ( 'NONE',  ( -1.062992125984252079, 0.5905511811023621549, -1.014069264286642236 ) ) ;
#11568=ORIENTED_EDGE ( 'NONE', *, *, #44486, .F. ) ;
#11572=EDGE_CURVE ( 'NONE', #26402, #38556, #22485, .T. ) ;
#11577=DIRECTION ( 'NONE',  ( -0.7071067811865466846, -0.7071067811865483499, -6.409875621278517705E-17 ) ) ;
#11643=CARTESIAN_POINT ( 'NONE',  ( -0.6529837180168072130, 0.8335264911517247244, 0.6529837180168073241 ) ) ;
#11681=ORIENTED_EDGE ( 'NONE', *, *, #28818, .T. ) ;
#11689=ORIENTED_EDGE ( 'NONE', *, *, #35623, .F. ) ;
#11714=ORIENTED_EDGE ( 'NONE', *, *, #39841, .F. ) ;
#11746=CARTESIAN_POINT ( 'NONE',  ( 0.6529837180168055477, 0.8335264911517253905, -0.6529837180168074351 ) ) ;
#11788=LINE ( 'NONE', #35041, #29570 ) ;
#11843=DIRECTION ( 'NONE',  ( -0.000000000000000000, -1.000000000000000000, -0.000000000000000000 ) ) ;
#11890=CARTESIAN_POINT ( 'NONE',  ( 1.025452293874513643, 0.4349011127721510994, 1.051609096396380005 ) ) ;
#11938=AXIS2_PLACEMENT_3D ( 'NONE', #3387, #4148, #22761 ) ;
#12139=VERTEX_POINT ( 'NONE', #36276 ) ;
#12174=ORIENTED_EDGE ( 'NONE', *, *, #2417, .T. ) ;
#12339=PLANE ( 'NONE',  #49294 ) ;
#12496=CARTESIAN_POINT ( 'NONE',  ( -1.062992125984251413, 0.000000000000000000, -1.181102362204724754 ) ) ;
#12541=DIRECTION ( 'NONE',  ( 0.000000000000000000, -0.000000000000000000, 1.000000000000000000 ) ) ;
#12587=DIRECTION ( 'NONE',  ( -0.7071067811865483499, -1.442222014787672788E-15, -0.7071067811865465735 ) ) ;
#12622=CARTESIAN_POINT ( 'NONE',  ( -1.062992125984252079, 0.5905511811023621549, -1.181102362204724754 ) ) ;
#12636=DIRECTION ( 'NONE',  ( -1.000000000000000000, 0.000000000000000000, 0.000000000000000000 ) ) ;
#12817=DIRECTION ( 'NONE',  ( -2.200518442539857142E-16, 0.7071067811865483499, 0.7071067811865465735 ) ) ;
#13164=EDGE_CURVE ( 'NONE', #49043, #30631, #943, .T. ) ;
#13198=EDGE_CURVE ( 'NONE', #14529, #23981, #32718, .T. ) ;
#13203=ORIENTED_EDGE ( 'NONE', *, *, #35072, .F. ) ;
#13309=VECTOR ( 'NONE', #37336, 39.37007874015748854 ) ;
#13362=ORIENTED_EDGE ( 'NONE', *, *, #31887, .T. ) ;
#13433=ORIENTED_EDGE ( 'NONE', *, *, #11208, .F. ) ;
#13451=CARTESIAN_POINT ( 'NONE',  ( -1.181102362204724088, 0.5905511811023621549, 1.181102362204724088 ) ) ;
#13474=VERTEX_POINT ( 'NONE', #22602 ) ;
#13498=DIRECTION ( 'NONE',  ( -1.000000000000000000, 0.000000000000000000, 0.000000000000000000 ) ) ;
#13650=DIRECTION ( 'NONE',  ( -1.156482317317871478E-16, 0.000000000000000000, -1.000000000000000000 ) ) ;
#13723=ADVANCED_FACE ( 'NONE', ( #39202 ), #15460, .F. ) ;
#13732=ORIENTED_EDGE ( 'NONE', *, *, #37352, .F. ) ;
#13801=PLANE ( 'NONE',  #17884 ) ;
#13817=CARTESIAN_POINT ( 'NONE',  ( 0.9948011493083116497, 0.5223602044264220590, 0.9948011493083110945 ) ) ;
#13834=LINE ( 'NONE', #45549, #13309 ) ;
#13850=LINE ( 'NONE', #2232, #22627 ) ;
#13909=DIRECTION ( 'NONE',  ( 0.7071067811865469066, 0.7071067811865481278, -4.088782444488994004E-17 ) ) ;
#13924=ADVANCED_FACE ( 'NONE', ( #1743 ), #2004, .F. ) ;
#13929=ORIENTED_EDGE ( 'NONE', *, *, #45938, .F. ) ;
#13985=ORIENTED_EDGE ( 'NONE', *, *, #14575, .F. ) ;
#14006=PLANE ( 'NONE',  #39316 ) ;
#14028=ORIENTED_EDGE ( 'NONE', *, *, #38933, .F. ) ;
#14055=EDGE_CURVE ( 'NONE', #30221, #30309, #3781, .T. ) ;
#14056=CARTESIAN_POINT ( 'NONE',  ( -1.025452293874513199, 0.4610579152940182390, -1.025452293874513865 ) ) ;
#14151=ADVANCED_FACE ( 'NONE', ( #43764 ), #4037, .T. ) ;
#14156=VECTOR ( 'NONE', #19463, 39.37007874015748143 ) ;
#14194=CARTESIAN_POINT ( 'NONE',  ( 1.014069264286641570, 0.000000000000000000, -1.062992125984252301 ) ) ;
#14316=DIRECTION ( 'NONE',  ( 0.000000000000000000, -0.7071067811865479058, 0.7071067811865470176 ) ) ;
#14327=CARTESIAN_POINT ( 'NONE',  ( -1.014069264286641570, 0.4235180831842794702, -1.062992125984252301 ) ) ;
#14341=ORIENTED_EDGE ( 'NONE', *, *, #14055, .T. ) ;
#14386=CARTESIAN_POINT ( 'NONE',  ( -1.038530695135446713, 0.4479795140330846137, 1.025452293874513199 ) ) ;
#14446=DIRECTION ( 'NONE',  ( 0.000000000000000000, 0.7071067811865482389, 0.7071067811865467956 ) ) ;
#14529=VERTEX_POINT ( 'NONE', #10960 ) ;
#14571=DIRECTION ( 'NONE',  ( 1.442222014787672788E-15, -0.7071067811865483499, -0.7071067811865465735 ) ) ;
#14575=EDGE_CURVE ( 'NONE', #10297, #26402, #18201, .T. ) ;
#14593=VERTEX_POINT ( 'NONE', #14327 ) ;
#14626=ORIENTED_EDGE ( 'NONE', *, *, #36635, .F. ) ;
#14735=LINE ( 'NONE', #3362, #36149 ) ;
#14896=EDGE_CURVE ( 'NONE', #22491, #7253, #22515, .T. ) ;
#14966=LINE ( 'NONE', #7226, #38200 ) ;
#15056=ORIENTED_EDGE ( 'NONE', *, *, #41949, .T. ) ;
#15097=PLANE ( 'NONE',  #47893 ) ;
#15125=DIRECTION ( 'NONE',  ( -0.5773502691896259531, 0.5773502691896245098, -0.5773502691896270633 ) ) ;
#15259=EDGE_CURVE ( 'NONE', #32429, #20197, #35285, .T. ) ;
#15336=ORIENTED_EDGE ( 'NONE', *, *, #14055, .F. ) ;
#15342=DIRECTION ( 'NONE',  ( -1.156482317317871478E-16, 0.000000000000000000, -1.000000000000000000 ) ) ;
#15456=EDGE_LOOP ( 'NONE', ( #38456, #11324, #23619 ) ) ;
#15460=PLANE ( 'NONE',  #44973 ) ;
#15495=VECTOR ( 'NONE', #20510, 39.37007874015748143 ) ;
#15512=EDGE_LOOP ( 'NONE', ( #33763, #1541, #50946, #27897, #51003, #47122 ) ) ;
#15553=LINE ( 'NONE', #7800, #31982 ) ;
#15605=LINE ( 'NONE', #47053, #50810 ) ;
#15705=PLANE ( 'NONE',  #22122 ) ;
#15750=LINE ( 'NONE', #47206, #8918 ) ;
#15869=VECTOR ( 'NONE', #32353, 39.37007874015748143 ) ;
#15881=PLANE ( 'NONE',  #34058 ) ;
#15926=DIRECTION ( 'NONE',  ( -0.7071067811865483499, 0.7071067811865466846, 8.177564888978005264E-17 ) ) ;
#15982=ADVANCED_FACE ( 'NONE', ( #48830 ), #25634, .T. ) ;
#15985=AXIS2_PLACEMENT_3D ( 'NONE', #8628, #3737, #39613 ) ;
#16013=( GEOMETRIC_REPRESENTATION_CONTEXT ( 3 ) GLOBAL_UNCERTAINTY_ASSIGNED_CONTEXT ( ( #9178 ) ) GLOBAL_UNIT_ASSIGNED_CONTEXT ( ( #50817, #2887, #34633 ) ) REPRESENTATION_CONTEXT ( 'NONE', 'WORKASPACE' ) );
#16101=VECTOR ( 'NONE', #42098, 39.37007874015748143 ) ;
#16118=PLANE ( 'NONE',  #15985 ) ;
#16141=LINE ( 'NONE', #16399, #33919 ) ;
#16204=ADVANCED_FACE ( 'NONE', ( #30276 ), #49591, .F. ) ;
#16278=ADVANCED_FACE ( 'NONE', ( #19390 ), #24557, .T. ) ;
#16399=CARTESIAN_POINT ( 'NONE',  ( -0.7317238754971217007, 0.1411726943947596014, -1.345337514773771614 ) ) ;
#16464=LINE ( 'NONE', #47913, #33910 ) ;
#16526=DIRECTION ( 'NONE',  ( 0.5773502691896241767, 0.5773502691896261751, 0.5773502691896268413 ) ) ;
#16543=VECTOR ( 'NONE', #23816, 39.37007874015748143 ) ;
#16597=CARTESIAN_POINT ( 'NONE',  ( 1.062992125984252079, 0.4235180831842795257, -1.014069264286642014 ) ) ;
#16628=CARTESIAN_POINT ( 'NONE',  ( 1.345337514773771614, 0.1411726943947604063, -0.7317238754971229220 ) ) ;
#16679=ORIENTED_EDGE ( 'NONE', *, *, #18637, .F. ) ;
#16683=DIRECTION ( 'NONE',  ( 0.000000000000000000, 1.000000000000000000, 0.000000000000000000 ) ) ;
#16701=EDGE_CURVE ( 'NONE', #30309, #43045, #43077, .T. ) ;
#16785=ADVANCED_FACE ( 'NONE', ( #36378 ), #33279, .T. ) ;
#16811=CARTESIAN_POINT ( 'NONE',  ( -1.062992125984251857, 0.4235180831842794702, 1.229331597148918448E-16 ) ) ;
#16821=PRODUCT_DEFINITION ( 'UNKNOWN', '', #45664, #6589 ) ;
#16847=CARTESIAN_POINT ( 'NONE',  ( -1.062992125984250968, 0.4724409448818890911, 1.181102362204724088 ) ) ;
#16928=ORIENTED_EDGE ( 'NONE', *, *, #26070, .F. ) ;
#16946=LINE ( 'NONE', #9189, #18756 ) ;
#17043=ORIENTED_EDGE ( 'NONE', *, *, #38272, .T. ) ;
#17053=APPLICATION_CONTEXT ( 'automotive_design' ) ;
#17087=DIRECTION ( 'NONE',  ( 0.000000000000000000, -1.000000000000000000, 0.000000000000000000 ) ) ;
#17124=ORIENTED_EDGE ( 'NONE', *, *, #38933, .T. ) ;
#17194=ADVANCED_FACE ( 'NONE', ( #35140 ), #31010, .T. ) ;
#17210=VERTEX_POINT ( 'NONE', #11890 ) ;
#17287=EDGE_LOOP ( 'NONE', ( #49560, #9461, #37404 ) ) ;
#17324=VECTOR ( 'NONE', #19320, 39.37007874015748143 ) ;
#17325=VECTOR ( 'NONE', #33952, 39.37007874015748143 ) ;
#17449=CARTESIAN_POINT ( 'NONE',  ( 1.025452293874513421, 0.4610579152940180725, 1.025452293874513199 ) ) ;
#17592=CARTESIAN_POINT ( 'NONE',  ( 1.181102362204724532, 0.5905511811023621549, 1.062992125984251413 ) ) ;
#17802=LINE ( 'NONE', #5924, #29516 ) ;
#17846=EDGE_CURVE ( 'NONE', #30518, #20081, #45568, .T. ) ;
#17884=AXIS2_PLACEMENT_3D ( 'NONE', #18179, #50128, #29546 ) ;
#18054=ADVANCED_FACE ( 'NONE', ( #638 ), #5272, .F. ) ;
#18060=ORIENTED_EDGE ( 'NONE', *, *, #21245, .T. ) ;
#18179=CARTESIAN_POINT ( 'NONE',  ( 1.062992125984251413, 0.5905511811023621549, -6.146657985744589776E-17 ) ) ;
#18201=LINE ( 'NONE', #33962, #33552 ) ;
#18251=ORIENTED_EDGE ( 'NONE', *, *, #47172, .F. ) ;
#18283=CARTESIAN_POINT ( 'NONE',  ( 0.9794755770252103755, 0.5070346321433210068, -5.663730925371873532E-17 ) ) ;
#18425=CARTESIAN_POINT ( 'NONE',  ( -1.025452293874513199, 0.4349011127721510994, -1.051609096396380671 ) ) ;
#18480=ORIENTED_EDGE ( 'NONE', *, *, #2245, .T. ) ;
#18541=CARTESIAN_POINT ( 'NONE',  ( 1.122047244094487972, 0.4724409448818892576, 1.122047244094487750 ) ) ;
#18637=EDGE_CURVE ( 'NONE', #21915, #14529, #3305, .T. ) ;
#18651=DIRECTION ( 'NONE',  ( 1.156482317317871478E-16, -0.000000000000000000, 1.000000000000000000 ) ) ;
#18666=CARTESIAN_POINT ( 'NONE',  ( 1.062992125984252079, 0.5905511811023621549, -1.014069264286642014 ) ) ;
#18717=VECTOR ( 'NONE', #2659, 39.37007874015748143 ) ;
#18756=VECTOR ( 'NONE', #23914, 39.37007874015748143 ) ;
#18855=CARTESIAN_POINT ( 'NONE',  ( 1.181102362204724310, 0.5905511811023621549, -1.181102362204724754 ) ) ;
#18983=EDGE_CURVE ( 'NONE', #41982, #47028, #26736, .T. ) ;
#19047=CARTESIAN_POINT ( 'NONE',  ( 1.097585813245683717, 0.000000000000000000, 0.9794755770252102645 ) ) ;
#19125=LENGTH_MEASURE_WITH_UNIT ( LENGTH_MEASURE( 0.02539999999999999897 ), #26623 );
#19149=VECTOR ( 'NONE', #49885, 39.37007874015748143 ) ;
#19171=ORIENTED_EDGE ( 'NONE', *, *, #35471, .F. ) ;
#19239=PLANE ( 'NONE',  #42916 ) ;
#19288=EDGE_LOOP ( 'NONE', ( #33853, #21730, #9731, #49504 ) ) ;
#19317=DIRECTION ( 'NONE',  ( 0.7071067811865486830, 0.000000000000000000, 0.7071067811865462405 ) ) ;
#19320=DIRECTION ( 'NONE',  ( 0.7071067811865483499, -0.000000000000000000, 0.7071067811865466846 ) ) ;
#19390=FACE_OUTER_BOUND ( 'NONE', #5247, .T. ) ;
#19393=ADVANCED_FACE ( 'NONE', ( #22309 ), #13801, .T. ) ;
#19463=DIRECTION ( 'NONE',  ( -0.7071067811865481278, 0.7071067811865469066, -1.221861889385012670E-15 ) ) ;
#19627=EDGE_LOOP ( 'NONE', ( #1937, #32321, #48950 ) ) ;
#19632=ORIENTED_EDGE ( 'NONE', *, *, #33029, .F. ) ;
#19686=EDGE_CURVE ( 'NONE', #13474, #2075, #43933, .T. ) ;
#19852=EDGE_LOOP ( 'NONE', ( #46850, #44757, #43040, #18480, #49434, #8039, #39814, #48591 ) ) ;
#19861=DIRECTION ( 'NONE',  ( 0.000000000000000000, -0.7071067811865479058, 0.7071067811865470176 ) ) ;
#19893=FACE_OUTER_BOUND ( 'NONE', #10473, .T. ) ;
#19998=DIRECTION ( 'NONE',  ( -0.000000000000000000, -1.000000000000000000, -0.000000000000000000 ) ) ;
#20010=ORIENTED_EDGE ( 'NONE', *, *, #39006, .F. ) ;
#20081=VERTEX_POINT ( 'NONE', #10945 ) ;
#20104=EDGE_CURVE ( 'NONE', #4657, #48594, #49881, .T. ) ;
#20197=VERTEX_POINT ( 'NONE', #4207 ) ;
#20295=CARTESIAN_POINT ( 'NONE',  ( -1.181102362204724310, 0.4724409448818890911, -1.062992125984252079 ) ) ;
#20313=PLANE ( 'NONE',  #45705 ) ;
#20317=ORIENTED_EDGE ( 'NONE', *, *, #33657, .T. ) ;
#20335=VECTOR ( 'NONE', #22329, 39.37007874015748854 ) ;
#20434=ORIENTED_EDGE ( 'NONE', *, *, #27123, .F. ) ;
#20467=DIRECTION ( 'NONE',  ( 0.000000000000000000, 0.000000000000000000, 1.000000000000000000 ) ) ;
#20510=DIRECTION ( 'NONE',  ( 0.7071067811865483499, -0.000000000000000000, -0.7071067811865466846 ) ) ;
#20538=VECTOR ( 'NONE', #7793, 39.37007874015748143 ) ;
#20542=LINE ( 'NONE', #28277, #47491 ) ;
#20556=CARTESIAN_POINT ( 'NONE',  ( 1.025452293874513421, 0.3889243959228481651, -1.097585813245683717 ) ) ;
#20618=EDGE_CURVE ( 'NONE', #10297, #45101, #25523, .T. ) ;
#20716=CARTESIAN_POINT ( 'NONE',  ( 0.000000000000000000, 0.4235180831842794702, -1.062992125984252301 ) ) ;
#20725=ADVANCED_FACE ( 'NONE', ( #29658, #34046 ), #2544, .F. ) ;
#20734=CARTESIAN_POINT ( 'NONE',  ( -1.062992125984252079, 0.000000000000000000, -1.014069264286642014 ) ) ;
#20830=DIRECTION ( 'NONE',  ( -1.156482317317871478E-16, 0.000000000000000000, -1.000000000000000000 ) ) ;
#20874=DIRECTION ( 'NONE',  ( 1.000000000000000000, 0.000000000000000000, -1.156482317317871478E-16 ) ) ;
#20876=DIMENSIONAL_EXPONENTS ( 1.000000000000000000, 0.000000000000000000, 0.000000000000000000, 0.000000000000000000, 0.000000000000000000, 0.000000000000000000, 0.000000000000000000 ) ;
#20910=EDGE_CURVE ( 'NONE', #49043, #26202, #20542, .T. ) ;
#20984=CARTESIAN_POINT ( 'NONE',  ( 0.000000000000000000, 0.000000000000000000, 0.000000000000000000 ) ) ;
#21103=ORIENTED_EDGE ( 'NONE', *, *, #20910, .F. ) ;
#21121=CARTESIAN_POINT ( 'NONE',  ( 0.000000000000000000, 0.4724409448818898127, 0.000000000000000000 ) ) ;
#21245=EDGE_CURVE ( 'NONE', #48594, #23441, #6587, .T. ) ;
#21273=LINE ( 'NONE', #1645, #49382 ) ;
#21416=ADVANCED_FACE ( 'NONE', ( #48567 ), #14006, .T. ) ;
#21471=ORIENTED_EDGE ( 'NONE', *, *, #45938, .T. ) ;
#21479=EDGE_CURVE ( 'NONE', #3209, #48480, #48813, .T. ) ;
#21487=CARTESIAN_POINT ( 'NONE',  ( -1.062992125984251635, 0.000000000000000000, 1.014069264286641570 ) ) ;
#21497=ORIENTED_EDGE ( 'NONE', *, *, #32466, .T. ) ;
#21502=ORIENTED_EDGE ( 'NONE', *, *, #854, .T. ) ;
#21522=DIRECTION ( 'NONE',  ( -0.7071067811865466846, -0.7071067811865483499, -6.409875621278517705E-17 ) ) ;
#21570=VECTOR ( 'NONE', #46951, 39.37007874015748143 ) ;
#21585=VERTEX_POINT ( 'NONE', #38018 ) ;
#21667=EDGE_CURVE ( 'NONE', #30309, #32429, #270, .T. ) ;
#21687=ORIENTED_EDGE ( 'NONE', *, *, #35919, .T. ) ;
#21730=ORIENTED_EDGE ( 'NONE', *, *, #19686, .F. ) ;
#21822=AXIS2_PLACEMENT_3D ( 'NONE', #43691, #40357, #31586 ) ;
#21846=DIRECTION ( 'NONE',  ( -0.000000000000000000, 1.000000000000000000, -0.000000000000000000 ) ) ;
#21874=ORIENTED_EDGE ( 'NONE', *, *, #28876, .F. ) ;
#21915=VERTEX_POINT ( 'NONE', #2578 ) ;
#21945=CARTESIAN_POINT ( 'NONE',  ( 1.062992125984251413, 0.5905511811023621549, 1.062992125984251413 ) ) ;
#22122=AXIS2_PLACEMENT_3D ( 'NONE', #6952, #39199, #43056 ) ;
#22153=VECTOR ( 'NONE', #12636, 39.37007874015748143 ) ;
#22257=CARTESIAN_POINT ( 'NONE',  ( 1.025452293874513421, 0.4349011127721513215, -1.051609096396380671 ) ) ;
#22309=FACE_OUTER_BOUND ( 'NONE', #35052, .T. ) ;
#22329=DIRECTION ( 'NONE',  ( -0.7071067811865483499, -2.200518442539857142E-16, 0.7071067811865465735 ) ) ;
#22371=ADVANCED_FACE ( 'NONE', ( #2708 ), #34712, .T. ) ;
#22373=ORIENTED_EDGE ( 'NONE', *, *, #16701, .T. ) ;
#22379=EDGE_CURVE ( 'NONE', #7604, #8873, #22580, .T. ) ;
#22460=( NAMED_UNIT ( * ) PLANE_ANGLE_UNIT ( ) SI_UNIT ( $, .RADIAN. ) );
#22474=FACE_OUTER_BOUND ( 'NONE', #10219, .T. ) ;
#22477=VERTEX_POINT ( 'NONE', #27709 ) ;
#22485=LINE ( 'NONE', #10612, #16101 ) ;
#22491=VERTEX_POINT ( 'NONE', #20734 ) ;
#22515=LINE ( 'NONE', #46235, #4346 ) ;
#22517=VECTOR ( 'NONE', #2584, 39.37007874015748143 ) ;
#22519=DIRECTION ( 'NONE',  ( -0.000000000000000000, 1.000000000000000000, -0.000000000000000000 ) ) ;
#22524=DIRECTION ( 'NONE',  ( -1.000000000000000000, 0.000000000000000000, 0.000000000000000000 ) ) ;
#22533=ORIENTED_EDGE ( 'NONE', *, *, #13198, .T. ) ;
#22580=LINE ( 'NONE', #38341, #47341 ) ;
#22602=CARTESIAN_POINT ( 'NONE',  ( -1.181102362204724310, 0.4724409448818890911, -1.062992125984252079 ) ) ;
#22627=VECTOR ( 'NONE', #45067, 39.37007874015748143 ) ;
#22727=DIRECTION ( 'NONE',  ( -1.000000000000000000, 0.000000000000000000, 5.782411586589357392E-17 ) ) ;
#22728=PLANE ( 'NONE',  #37738 ) ;
#22761=DIRECTION ( 'NONE',  ( -0.7071067811865482389, 0.000000000000000000, 0.7071067811865467956 ) ) ;
#22763=VECTOR ( 'NONE', #24555, 39.37007874015748854 ) ;
#22768=VECTOR ( 'NONE', #42643, 39.37007874015748143 ) ;
#22797=ORIENTED_EDGE ( 'NONE', *, *, #36855, .T. ) ;
#22829=DIRECTION ( 'NONE',  ( 1.000000000000000000, 0.000000000000000000, 0.000000000000000000 ) ) ;
#22975=EDGE_LOOP ( 'NONE', ( #49223, #39394, #16679, #21502, #13732, #21687, #11689, #333 ) ) ;
#22976=PLANE ( 'NONE',  #47223 ) ;
#23180=FACE_OUTER_BOUND ( 'NONE', #28936, .T. ) ;
#23213=CARTESIAN_POINT ( 'NONE',  ( 1.097585813245683717, 0.5905511811023621549, 0.9794755770252102645 ) ) ;
#23441=VERTEX_POINT ( 'NONE', #5882 ) ;
#23459=LINE ( 'NONE', #10838, #5855 ) ;
#23496=ORIENTED_EDGE ( 'NONE', *, *, #19686, .T. ) ;
#23501=VECTOR ( 'NONE', #5846, 39.37007874015748854 ) ;
#23619=ORIENTED_EDGE ( 'NONE', *, *, #4328, .F. ) ;
#23714=ORIENTED_EDGE ( 'NONE', *, *, #42644, .T. ) ;
#23767=ORIENTED_EDGE ( 'NONE', *, *, #50916, .T. ) ;
#23785=EDGE_LOOP ( 'NONE', ( #36082, #19171, #9115, #27506 ) ) ;
#23811=EDGE_LOOP ( 'NONE', ( #35090, #11050, #14341, #34565, #37955, #26264, #21497, #45028 ) ) ;
#23816=DIRECTION ( 'NONE',  ( 1.606762707810401785E-15, -0.7071067811865483499, 0.7071067811865466846 ) ) ;
#23847=EDGE_CURVE ( 'NONE', #47727, #25120, #30020, .T. ) ;
#23914=DIRECTION ( 'NONE',  ( 0.7071067811865483499, -0.000000000000000000, 0.7071067811865466846 ) ) ;
#23921=ORIENTED_EDGE ( 'NONE', *, *, #43831, .F. ) ;
#23923=CARTESIAN_POINT ( 'NONE',  ( 1.062992125984251413, 0.4724409448818890911, -1.181102362204724754 ) ) ;
#23929=EDGE_CURVE ( 'NONE', #12139, #50226, #31033, .T. ) ;
#23973=EDGE_CURVE ( 'NONE', #50189, #14529, #30780, .T. ) ;
#23981=VERTEX_POINT ( 'NONE', #39031 ) ;
#23983=ORIENTED_EDGE ( 'NONE', *, *, #13164, .F. ) ;
#24045=VECTOR ( 'NONE', #4231, 39.37007874015748854 ) ;
#24053=EDGE_CURVE ( 'NONE', #30992, #20081, #36184, .T. ) ;
#24179=AXIS2_PLACEMENT_3D ( 'NONE', #2832, #9563, #33324 ) ;
#24283=ORIENTED_EDGE ( 'NONE', *, *, #8055, .T. ) ;
#24288=DIRECTION ( 'NONE',  ( -0.5773502691896252870, -0.5773502691896267303, 0.5773502691896252870 ) ) ;
#24336=ORIENTED_EDGE ( 'NONE', *, *, #43107, .F. ) ;
#24376=CARTESIAN_POINT ( 'NONE',  ( 1.062992125984251635, 0.000000000000000000, 1.181102362204724088 ) ) ;
#24382=LINE ( 'NONE', #40137, #15495 ) ;
#24492=CARTESIAN_POINT ( 'NONE',  ( -1.062992125984250968, 0.000000000000000000, 1.181102362204724088 ) ) ;
#24541=ORIENTED_EDGE ( 'NONE', *, *, #3358, .F. ) ;
#24555=DIRECTION ( 'NONE',  ( 0.5773502691896268413, -0.5773502691896258421, 0.5773502691896243988 ) ) ;
#24557=PLANE ( 'NONE',  #45639 ) ;
#24607=CARTESIAN_POINT ( 'NONE',  ( 1.062992125984251413, 0.4724409448818890911, -1.181102362204724754 ) ) ;
#24608=CARTESIAN_POINT ( 'NONE',  ( 1.062992125984251413, 0.5905511811023621549, -1.181102362204724754 ) ) ;
#24646=CARTESIAN_POINT ( 'NONE',  ( -1.062992125984250968, 0.5905511811023621549, 1.181102362204724088 ) ) ;
#24700=CARTESIAN_POINT ( 'NONE',  ( -1.181102362204724310, 0.5905511811023621549, -1.062992125984252079 ) ) ;
#24711=CARTESIAN_POINT ( 'NONE',  ( -1.062992125984250968, 0.4724409448818890911, 1.181102362204724088 ) ) ;
#24834=DIMENSIONAL_EXPONENTS ( 1.000000000000000000, 0.000000000000000000, 0.000000000000000000, 0.000000000000000000, 0.000000000000000000, 0.000000000000000000, 0.000000000000000000 ) ;
#24854=LINE ( 'NONE', #20716, #15869 ) ;
#24900=EDGE_LOOP ( 'NONE', ( #49943, #32913, #22373, #43160, #29357, #49252, #41629, #17124 ) ) ;
#25029=CARTESIAN_POINT ( 'NONE',  ( 1.051609096396380227, 0.4349011127721513215, -1.025452293874513865 ) ) ;
#25120=VERTEX_POINT ( 'NONE', #49963 ) ;
#25325=EDGE_CURVE ( 'NONE', #38556, #8556, #16946, .T. ) ;
#25423=CARTESIAN_POINT ( 'NONE',  ( 0.9794755770252102645, 0.5905511811023621549, -1.097585813245683717 ) ) ;
#25523=LINE ( 'NONE', #758, #43353 ) ;
#25527=ORIENTED_EDGE ( 'NONE', *, *, #4473, .T. ) ;
#25634=PLANE ( 'NONE',  #27485 ) ;
#25864=ADVANCED_FACE ( 'NONE', ( #50095 ), #11151, .F. ) ;
#25926=ORIENTED_EDGE ( 'NONE', *, *, #47562, .F. ) ;
#25942=LINE ( 'NONE', #6829, #17325 ) ;
#26006=DIRECTION ( 'NONE',  ( 0.000000000000000000, 1.000000000000000000, 0.000000000000000000 ) ) ;
#26070=EDGE_CURVE ( 'NONE', #43045, #39291, #805, .T. ) ;
#26075=ORIENTED_EDGE ( 'NONE', *, *, #7827, .T. ) ;
#26142=LINE ( 'NONE', #30015, #28328 ) ;
#26143=DIRECTION ( 'NONE',  ( 0.000000000000000000, -1.000000000000000000, 0.000000000000000000 ) ) ;
#26202=VERTEX_POINT ( 'NONE', #48260 ) ;
#26206=DIRECTION ( 'NONE',  ( 1.000000000000000000, 0.000000000000000000, 0.000000000000000000 ) ) ;
#26264=ORIENTED_EDGE ( 'NONE', *, *, #18983, .F. ) ;
#26279=MECHANICAL_DESIGN_GEOMETRIC_PRESENTATION_REPRESENTATION('',(#34540),#44432);
#26345=DIRECTION ( 'NONE',  ( 5.782411586589357392E-17, 0.000000000000000000, 1.000000000000000000 ) ) ;
#26349=DIRECTION ( 'NONE',  ( 0.7071067811865483499, -0.000000000000000000, -0.7071067811865466846 ) ) ;
#26366=DIRECTION ( 'NONE',  ( -5.782411586589357392E-17, 0.000000000000000000, -1.000000000000000000 ) ) ;
#26393=DIRECTION ( 'NONE',  ( 0.5773502691896261751, 0.5773502691896261751, -0.5773502691896248429 ) ) ;
#26402=VERTEX_POINT ( 'NONE', #23923 ) ;
#26491=CARTESIAN_POINT ( 'NONE',  ( -1.062992125984250968, 0.4724409448818890911, 1.181102362204724088 ) ) ;
#26532=DIRECTION ( 'NONE',  ( -2.200518442539857142E-16, 0.7071067811865483499, 0.7071067811865465735 ) ) ;
#26623=( LENGTH_UNIT ( ) NAMED_UNIT ( * ) SI_UNIT ( $, .METRE. ) );
#26736=LINE ( 'NONE', #50187, #45826 ) ;
#26741=AXIS2_PLACEMENT_3D ( 'NONE', #20984, #20467, #36229 ) ;
#26748=EDGE_LOOP ( 'NONE', ( #48099, #44631, #43149 ) ) ;
#26758=EDGE_CURVE ( 'NONE', #30631, #13474, #15605, .T. ) ;
#26997=EDGE_LOOP ( 'NONE', ( #30574, #30483, #36118, #11262, #20317, #16928, #33226, #28239 ) ) ;
#27011=DIRECTION ( 'NONE',  ( 1.606762707810401785E-15, -0.7071067811865483499, 0.7071067811865466846 ) ) ;
#27014=LINE ( 'NONE', #49970, #950 ) ;
#27123=EDGE_CURVE ( 'NONE', #43045, #21585, #35165, .T. ) ;
#27197=CARTESIAN_POINT ( 'NONE',  ( -1.097585813245683273, 0.4349011127721510994, -0.9794755770252108196 ) ) ;
#27310=CARTESIAN_POINT ( 'NONE',  ( -0.9794755770252101534, 0.4349011127721510994, 1.097585813245683051 ) ) ;
#27311=DIRECTION ( 'NONE',  ( 0.5773502691896245098, 0.5773502691896259531, -0.5773502691896270633 ) ) ;
#27316=VECTOR ( 'NONE', #47878, 39.37007874015748854 ) ;
#27480=ADVANCED_FACE ( 'NONE', ( #42835 ), #22728, .F. ) ;
#27485=AXIS2_PLACEMENT_3D ( 'NONE', #44731, #9381, #41388 ) ;
#27493=CARTESIAN_POINT ( 'NONE',  ( -1.112911385528784214, 0.4042499682059492172, -0.9948011493083117607 ) ) ;
#27506=ORIENTED_EDGE ( 'NONE', *, *, #2417, .F. ) ;
#27709=CARTESIAN_POINT ( 'NONE',  ( -1.014069264286641570, 0.4235180831842794702, 1.062992125984251635 ) ) ;
#27801=EDGE_LOOP ( 'NONE', ( #25527, #50825, #6496, #64 ) ) ;
#27818=FACE_OUTER_BOUND ( 'NONE', #15512, .T. ) ;
#27848=CARTESIAN_POINT ( 'NONE',  ( 0.000000000000000000, 0.4724409448818898127, 1.014069264286641570 ) ) ;
#27849=AXIS2_PLACEMENT_3D ( 'NONE', #32509, #20874, #5382 ) ;
#27897=ORIENTED_EDGE ( 'NONE', *, *, #6385, .T. ) ;
#27976=LINE ( 'NONE', #47817, #14156 ) ;
#28024=EDGE_LOOP ( 'NONE', ( #4375, #22533, #23714, #51016, #36208, #40035 ) ) ;
#28126=VECTOR ( 'NONE', #35332, 39.37007874015748854 ) ;
#28239=ORIENTED_EDGE ( 'NONE', *, *, #3358, .T. ) ;
#28277=CARTESIAN_POINT ( 'NONE',  ( 1.181102362204724532, 0.5905511811023621549, 1.062992125984251413 ) ) ;
#28328=VECTOR ( 'NONE', #22519, 39.37007874015748143 ) ;
#28415=DIRECTION ( 'NONE',  ( 0.7071067811865463515, 0.000000000000000000, -0.7071067811865487940 ) ) ;
#28552=LINE ( 'NONE', #47880, #32257 ) ;
#28664=VECTOR ( 'NONE', #1686, 39.37007874015748143 ) ;
#28726=ORIENTED_EDGE ( 'NONE', *, *, #28998, .F. ) ;
#28818=EDGE_CURVE ( 'NONE', #30940, #8556, #37964, .T. ) ;
#28876=EDGE_CURVE ( 'NONE', #7253, #41982, #14966, .T. ) ;
#28936=EDGE_LOOP ( 'NONE', ( #46099, #35390, #25926, #4858 ) ) ;
#28949=EDGE_LOOP ( 'NONE', ( #30864, #24541, #47568, #11568, #29196, #13929, #8054, #5357 ) ) ;
#28998=EDGE_CURVE ( 'NONE', #42546, #33385, #4612, .T. ) ;
#29064=PLANE ( 'NONE',  #33716 ) ;
#29094=ORIENTED_EDGE ( 'NONE', *, *, #20618, .F. ) ;
#29142=LINE ( 'NONE', #37165, #22153 ) ;
#29185=AXIS2_PLACEMENT_3D ( 'NONE', #13451, #4934, #32571 ) ;
#29196=ORIENTED_EDGE ( 'NONE', *, *, #20104, .T. ) ;
#29357=ORIENTED_EDGE ( 'NONE', *, *, #46300, .F. ) ;
#29419=LINE ( 'NONE', #9802, #37235 ) ;
#29433=ORIENTED_EDGE ( 'NONE', *, *, #40201, .T. ) ;
#29516=VECTOR ( 'NONE', #33569, 39.37007874015748143 ) ;
#29546=DIRECTION ( 'NONE',  ( 5.782411586589357392E-17, -0.000000000000000000, 1.000000000000000000 ) ) ;
#29561=DIRECTION ( 'NONE',  ( 0.5773502691896241767, 0.5773502691896261751, 0.5773502691896268413 ) ) ;
#29570=VECTOR ( 'NONE', #39159, 39.37007874015748143 ) ;
#29604=EDGE_CURVE ( 'NONE', #8748, #14593, #26142, .T. ) ;
#29658=FACE_BOUND ( 'NONE', #22975, .T. ) ;
#29669=DIRECTION ( 'NONE',  ( -0.7071067811865483499, -0.000000000000000000, 0.7071067811865466846 ) ) ;
#29699=( NAMED_UNIT ( * ) SI_UNIT ( $, .STERADIAN. ) SOLID_ANGLE_UNIT ( ) );
#29808=ADVANCED_FACE ( 'NONE', ( #49022 ), #9575, .F. ) ;
#29905=FACE_OUTER_BOUND ( 'NONE', #26997, .T. ) ;
#30015=CARTESIAN_POINT ( 'NONE',  ( -1.014069264286641570, 0.5905511811023621549, -1.062992125984252301 ) ) ;
#30020=LINE ( 'NONE', #20556, #31841 ) ;
#30110=VECTOR ( 'NONE', #44601, 39.37007874015748854 ) ;
#30161=CARTESIAN_POINT ( 'NONE',  ( 1.181102362204724310, 0.4724409448818893686, -1.062992125984252079 ) ) ;
#30178=VECTOR ( 'NONE', #48003, 39.37007874015748143 ) ;
#30181=VECTOR ( 'NONE', #50205, 39.37007874015748143 ) ;
#30221=VERTEX_POINT ( 'NONE', #41019 ) ;
#30276=FACE_OUTER_BOUND ( 'NONE', #24900, .T. ) ;
#30309=VERTEX_POINT ( 'NONE', #4620 ) ;
#30321=FACE_OUTER_BOUND ( 'NONE', #26748, .T. ) ;
#30483=ORIENTED_EDGE ( 'NONE', *, *, #39538, .F. ) ;
#30518=VERTEX_POINT ( 'NONE', #4058 ) ;
#30533=CARTESIAN_POINT ( 'NONE',  ( 1.030376884852512109, 0.4561333243160193840, 1.046684505418381539 ) ) ;
#30574=ORIENTED_EDGE ( 'NONE', *, *, #8055, .F. ) ;
#30597=FACE_OUTER_BOUND ( 'NONE', #33061, .T. ) ;
#30631=VERTEX_POINT ( 'NONE', #8944 ) ;
#30636=VERTEX_POINT ( 'NONE', #1200 ) ;
#30718=DIRECTION ( 'NONE',  ( 0.000000000000000000, -1.000000000000000000, 0.000000000000000000 ) ) ;
#30780=LINE ( 'NONE', #46491, #22768 ) ;
#30864=ORIENTED_EDGE ( 'NONE', *, *, #23847, .T. ) ;
#30877=DIRECTION ( 'NONE',  ( -0.7071067811865482389, 0.000000000000000000, 0.7071067811865467956 ) ) ;
#30904=CARTESIAN_POINT ( 'NONE',  ( -1.025452293874513199, 0.5070346321433201187, 0.9794755770252113747 ) ) ;
#30939=CARTESIAN_POINT ( 'NONE',  ( -1.181102362204724310, 0.5905511811023621549, -1.062992125984252301 ) ) ;
#30940=VERTEX_POINT ( 'NONE', #46565 ) ;
#30959=CARTESIAN_POINT ( 'NONE',  ( 0.9794755770252102645, 0.000000000000000000, -1.097585813245683717 ) ) ;
#30992=VERTEX_POINT ( 'NONE', #12496 ) ;
#31010=PLANE ( 'NONE',  #11938 ) ;
#31033=LINE ( 'NONE', #30533, #37600 ) ;
#31066=VERTEX_POINT ( 'NONE', #24376 ) ;
#31070=VECTOR ( 'NONE', #24288, 39.37007874015748143 ) ;
#31087=ORIENTED_EDGE ( 'NONE', *, *, #11572, .T. ) ;
#31158=LINE ( 'NONE', #11535, #6705 ) ;
#31169=ADVANCED_FACE ( 'NONE', ( #22474 ), #22976, .T. ) ;
#31204=PLANE ( 'NONE',  #48419 ) ;
#31253=ORIENTED_EDGE ( 'NONE', *, *, #26758, .T. ) ;
#31358=DIRECTION ( 'NONE',  ( -1.156482317317871478E-16, 0.000000000000000000, -1.000000000000000000 ) ) ;
#31376=LINE ( 'NONE', #11746, #11446 ) ;
#31412=DIRECTION ( 'NONE',  ( -1.000000000000000000, 0.000000000000000000, 0.000000000000000000 ) ) ;
#31485=ADVANCED_FACE ( 'NONE', ( #29905 ), #46378, .F. ) ;
#31558=CARTESIAN_POINT ( 'NONE',  ( -0.6529837180168073241, 0.8335264911517249464, -0.6529837180168078792 ) ) ;
#31586=DIRECTION ( 'NONE',  ( 1.000000000000000000, 0.000000000000000000, -0.000000000000000000 ) ) ;
#31650=DIRECTION ( 'NONE',  ( 1.000000000000000000, 0.000000000000000000, 0.000000000000000000 ) ) ;
#31716=FACE_OUTER_BOUND ( 'NONE', #45032, .T. ) ;
#31841=VECTOR ( 'NONE', #12817, 39.37007874015748854 ) ;
#31848=PLANE ( 'NONE',  #21822 ) ;
#31887=EDGE_CURVE ( 'NONE', #8556, #10297, #13850, .T. ) ;
#31888=CARTESIAN_POINT ( 'NONE',  ( -1.181102362204724310, 0.000000000000000000, -1.062992125984252079 ) ) ;
#31982=VECTOR ( 'NONE', #4181, 39.37007874015748143 ) ;
#32036=SHAPE_DEFINITION_REPRESENTATION ( #7091, #5020 ) ;
#32077=LINE ( 'NONE', #31558, #48610 ) ;
#32254=AXIS2_PLACEMENT_3D ( 'NONE', #4651, #16526, #19861 ) ;
#32257=VECTOR ( 'NONE', #31412, 39.37007874015748143 ) ;
#32313=CARTESIAN_POINT ( 'NONE',  ( -1.062992125984251413, 0.5905511811023621549, -1.181102362204724754 ) ) ;
#32321=ORIENTED_EDGE ( 'NONE', *, *, #7824, .T. ) ;
#32322=AXIS2_PLACEMENT_3D ( 'NONE', #30939, #7940, #191 ) ;
#32353=DIRECTION ( 'NONE',  ( 1.000000000000000000, -0.000000000000000000, 0.000000000000000000 ) ) ;
#32429=VERTEX_POINT ( 'NONE', #46973 ) ;
#32466=EDGE_CURVE ( 'NONE', #41982, #30636, #1052, .T. ) ;
#32479=VECTOR ( 'NONE', #22829, 39.37007874015748143 ) ;
#32509=CARTESIAN_POINT ( 'NONE',  ( -1.181102362204724310, 0.5905511811023621549, -1.181102362204724754 ) ) ;
#32525=DIRECTION ( 'NONE',  ( 5.782411586589357392E-17, 0.000000000000000000, 1.000000000000000000 ) ) ;
#32571=DIRECTION ( 'NONE',  ( -1.000000000000000000, 0.000000000000000000, -0.000000000000000000 ) ) ;
#32716=AXIS2_PLACEMENT_3D ( 'NONE', #49230, #3048, #38177 ) ;
#32718=LINE ( 'NONE', #48396, #11158 ) ;
#32775=ADVANCED_FACE ( 'NONE', ( #43073 ), #46678, .T. ) ;
#32818=CARTESIAN_POINT ( 'NONE',  ( -1.014069264286641570, 0.000000000000000000, -1.062992125984252301 ) ) ;
#32848=AXIS2_PLACEMENT_3D ( 'NONE', #13817, #29561, #14316 ) ;
#32868=ORIENTED_EDGE ( 'NONE', *, *, #4328, .T. ) ;
#32876=EDGE_LOOP ( 'NONE', ( #43696, #2799, #44630, #47712 ) ) ;
#32913=ORIENTED_EDGE ( 'NONE', *, *, #21667, .F. ) ;
#33018=DIRECTION ( 'NONE',  ( -0.7071067811865486830, 0.000000000000000000, -0.7071067811865462405 ) ) ;
#33029=EDGE_CURVE ( 'NONE', #30636, #23441, #41512, .T. ) ;
#33061=EDGE_LOOP ( 'NONE', ( #48032, #6682, #32868, #21103 ) ) ;
#33062=CARTESIAN_POINT ( 'NONE',  ( 1.014069264286641570, 0.4235180831842794702, -1.062992125984252301 ) ) ;
#33108=EDGE_LOOP ( 'NONE', ( #34617, #6721, #23983, #41442 ) ) ;
#33226=ORIENTED_EDGE ( 'NONE', *, *, #27123, .T. ) ;
#33279=PLANE ( 'NONE',  #6974 ) ;
#33304=CARTESIAN_POINT ( 'NONE',  ( 1.062992125984251413, 0.5905511811023621549, 1.062992125984251413 ) ) ;
#33322=EDGE_CURVE ( 'NONE', #50880, #30518, #28552, .T. ) ;
#33324=DIRECTION ( 'NONE',  ( -1.000000000000000000, 0.000000000000000000, -0.000000000000000000 ) ) ;
#33385=VERTEX_POINT ( 'NONE', #5320 ) ;
#33507=ORIENTED_EDGE ( 'NONE', *, *, #21479, .T. ) ;
#33552=VECTOR ( 'NONE', #49648, 39.37007874015748854 ) ;
#33569=DIRECTION ( 'NONE',  ( 0.7071067811865483499, 1.579007132194770110E-15, -0.7071067811865466846 ) ) ;
#33657=EDGE_CURVE ( 'NONE', #50226, #39291, #27976, .T. ) ;
#33708=CLOSED_SHELL ( 'NONE', ( #27480, #51007, #42695, #29808, #14151, #20725, #43208, #15982, #40296, #17194, #21416, #18054, #22371, #19393, #25864, #10524, #46227, #39412, #31169, #48943, #16785, #8979, #13924, #9715, #49526, #1391, #45779, #40023, #16278, #10461, #31485, #32775, #13723, #1501, #16204 ) ) ;
#33716=AXIS2_PLACEMENT_3D ( 'NONE', #24700, #44806, #4820 ) ;
#33762=LINE ( 'NONE', #26491, #43020 ) ;
#33763=ORIENTED_EDGE ( 'NONE', *, *, #37352, .T. ) ;
#33853=ORIENTED_EDGE ( 'NONE', *, *, #2245, .F. ) ;
#33902=EDGE_LOOP ( 'NONE', ( #43218, #38969, #13203 ) ) ;
#33910=VECTOR ( 'NONE', #12587, 39.37007874015748854 ) ;
#33919=VECTOR ( 'NONE', #48357, 39.37007874015748854 ) ;
#33952=DIRECTION ( 'NONE',  ( -0.7071067811865481278, 0.7071067811865469066, 4.592716591420704405E-16 ) ) ;
#33962=CARTESIAN_POINT ( 'NONE',  ( 1.062992125984251413, 0.4724409448818890911, -1.181102362204724754 ) ) ;
#34046=FACE_OUTER_BOUND ( 'NONE', #19852, .T. ) ;
#34058=AXIS2_PLACEMENT_3D ( 'NONE', #40159, #4781, #8907 ) ;
#34087=CARTESIAN_POINT ( 'NONE',  ( 1.181102362204724310, 0.000000000000000000, -1.181102362204724754 ) ) ;
#34180=EDGE_LOOP ( 'NONE', ( #2169, #2130, #2527 ) ) ;
#34268=ORIENTED_EDGE ( 'NONE', *, *, #50916, .F. ) ;
#34280=VECTOR ( 'NONE', #42159, 39.37007874015748143 ) ;
#34346=CARTESIAN_POINT ( 'NONE',  ( 1.062992125984251413, 0.000000000000000000, -1.181102362204724754 ) ) ;
#34540=STYLED_ITEM('',(#51073),#41217);
#34565=ORIENTED_EDGE ( 'NONE', *, *, #21667, .T. ) ;
#34606=DIRECTION ( 'NONE',  ( -1.000000000000000000, 0.000000000000000000, 5.782411586589357392E-17 ) ) ;
#34617=ORIENTED_EDGE ( 'NONE', *, *, #35072, .T. ) ;
#34633=( NAMED_UNIT ( * ) SI_UNIT ( $, .STERADIAN. ) SOLID_ANGLE_UNIT ( ) );
#34712=PLANE ( 'NONE',  #41603 ) ;
#34786=CARTESIAN_POINT ( 'NONE',  ( 1.014069264286641792, 0.4724409448818898127, 1.014069264286641570 ) ) ;
#34807=EDGE_LOOP ( 'NONE', ( #15336, #13433, #20434, #39776 ) ) ;
#34892=ORIENTED_EDGE ( 'NONE', *, *, #23847, .F. ) ;
#35041=CARTESIAN_POINT ( 'NONE',  ( -1.181102362204724088, 0.5905511811023621549, 1.062992125984251413 ) ) ;
#35052=EDGE_LOOP ( 'NONE', ( #15056, #14626, #11714, #29094 ) ) ;
#35072=EDGE_CURVE ( 'NONE', #30518, #13474, #21273, .T. ) ;
#35090=ORIENTED_EDGE ( 'NONE', *, *, #7824, .F. ) ;
#35140=FACE_OUTER_BOUND ( 'NONE', #33902, .T. ) ;
#35165=LINE ( 'NONE', #38041, #18717 ) ;
#35236=FACE_OUTER_BOUND ( 'NONE', #10233, .T. ) ;
#35264=CARTESIAN_POINT ( 'NONE',  ( 1.046684505418381761, 0.4561333243160196060, -1.030376884852512331 ) ) ;
#35285=LINE ( 'NONE', #30904, #2739 ) ;
#35332=DIRECTION ( 'NONE',  ( 0.7071067811865486830, 2.775557561562891351E-17, 0.7071067811865462405 ) ) ;
#35356=DIRECTION ( 'NONE',  ( -0.7071067811865466846, -0.000000000000000000, -0.7071067811865483499 ) ) ;
#35390=ORIENTED_EDGE ( 'NONE', *, *, #22379, .F. ) ;
#35413=PLANE ( 'NONE',  #27849 ) ;
#35471=EDGE_CURVE ( 'NONE', #45101, #30940, #1839, .T. ) ;
#35502=VERTEX_POINT ( 'NONE', #8820 ) ;
#35572=PLANE ( 'NONE',  #32322 ) ;
#35623=EDGE_CURVE ( 'NONE', #22491, #8748, #14735, .T. ) ;
#35682=DIRECTION ( 'NONE',  ( 0.5773502691896252870, 0.5773502691896266192, 0.5773502691896251759 ) ) ;
#35765=LINE ( 'NONE', #47851, #46098 ) ;
#35811=FACE_OUTER_BOUND ( 'NONE', #23811, .T. ) ;
#35880=CARTESIAN_POINT ( 'NONE',  ( -1.062992125984250968, 0.5905511811023621549, 1.181102362204724088 ) ) ;
#35919=EDGE_CURVE ( 'NONE', #8873, #8748, #29142, .T. ) ;
#36040=ORIENTED_EDGE ( 'NONE', *, *, #25325, .F. ) ;
#36082=ORIENTED_EDGE ( 'NONE', *, *, #46291, .F. ) ;
#36118=ORIENTED_EDGE ( 'NONE', *, *, #47172, .T. ) ;
#36149=VECTOR ( 'NONE', #26349, 39.37007874015748143 ) ;
#36184=LINE ( 'NONE', #32313, #30178 ) ;
#36208=ORIENTED_EDGE ( 'NONE', *, *, #23929, .F. ) ;
#36229=DIRECTION ( 'NONE',  ( 1.000000000000000000, 0.000000000000000000, 0.000000000000000000 ) ) ;
#36276=CARTESIAN_POINT ( 'NONE',  ( 1.062992125984252079, 0.4235180831842795257, 1.014069264286641792 ) ) ;
#36285=DIRECTION ( 'NONE',  ( 1.156482317317871478E-16, 0.000000000000000000, 1.000000000000000000 ) ) ;
#36378=FACE_OUTER_BOUND ( 'NONE', #10571, .T. ) ;
#36635=EDGE_CURVE ( 'NONE', #26202, #50880, #4984, .T. ) ;
#36741=DIRECTION ( 'NONE',  ( -5.782411586589357392E-17, 0.000000000000000000, -1.000000000000000000 ) ) ;
#36855=EDGE_CURVE ( 'NONE', #38556, #30992, #42125, .T. ) ;
#37165=CARTESIAN_POINT ( 'NONE',  ( -1.181102362204724310, 0.000000000000000000, -1.062992125984252301 ) ) ;
#37201=( CONVERSION_BASED_UNIT ( 'INCH', #41073 ) LENGTH_UNIT ( ) NAMED_UNIT ( #24834 ) );
#37235=VECTOR ( 'NONE', #1027, 39.37007874015748143 ) ;
#37253=ADVANCED_BREP_SHAPE_REPRESENTATION ( '', ( #41217, #26741 ), #16013 ) ;
#37336=DIRECTION ( 'NONE',  ( -0.7071067811865486830, 0.000000000000000000, -0.7071067811865462405 ) ) ;
#37352=EDGE_CURVE ( 'NONE', #8873, #35502, #3589, .T. ) ;
#37404=ORIENTED_EDGE ( 'NONE', *, *, #5898, .F. ) ;
#37511=DIRECTION ( 'NONE',  ( -1.000000000000000000, -0.000000000000000000, -0.000000000000000000 ) ) ;
#37600=VECTOR ( 'NONE', #6538, 39.37007874015748854 ) ;
#37634=AXIS2_PLACEMENT_3D ( 'NONE', #47355, #16683, #12541 ) ;
#37729=ORIENTED_EDGE ( 'NONE', *, *, #7827, .F. ) ;
#37738=AXIS2_PLACEMENT_3D ( 'NONE', #18855, #34606, #26345 ) ;
#37938=DIRECTION ( 'NONE',  ( -8.653332088726061579E-16, 0.7071067811865483499, -0.7071067811865466846 ) ) ;
#37955=ORIENTED_EDGE ( 'NONE', *, *, #40546, .T. ) ;
#37964=LINE ( 'NONE', #34087, #22517 ) ;
#38018=CARTESIAN_POINT ( 'NONE',  ( 1.014069264286641792, 0.4724409448818898127, -1.014069264286642236 ) ) ;
#38041=CARTESIAN_POINT ( 'NONE',  ( 1.014069264286641792, 0.4724409448818898127, -5.863765863415223092E-17 ) ) ;
#38177=DIRECTION ( 'NONE',  ( 0.000000000000000000, -0.000000000000000000, 1.000000000000000000 ) ) ;
#38200=VECTOR ( 'NONE', #3594, 39.37007874015748143 ) ;
#38272=EDGE_CURVE ( 'NONE', #42546, #31066, #45797, .T. ) ;
#38341=CARTESIAN_POINT ( 'NONE',  ( 1.014069264286641570, 0.5905511811023621549, -1.062992125984252301 ) ) ;
#38456=ORIENTED_EDGE ( 'NONE', *, *, #5511, .T. ) ;
#38554=EDGE_CURVE ( 'NONE', #22477, #50189, #23459, .T. ) ;
#38556=VERTEX_POINT ( 'NONE', #34346 ) ;
#38933=EDGE_CURVE ( 'NONE', #22477, #20197, #27014, .T. ) ;
#38949=VECTOR ( 'NONE', #42988, 39.37007874015748854 ) ;
#38969=ORIENTED_EDGE ( 'NONE', *, *, #39061, .T. ) ;
#38981=VECTOR ( 'NONE', #33018, 39.37007874015748854 ) ;
#39006=EDGE_CURVE ( 'NONE', #30636, #22491, #31158, .T. ) ;
#39026=CARTESIAN_POINT ( 'NONE',  ( -1.062992125984250968, 0.000000000000000000, 1.181102362204724088 ) ) ;
#39031=CARTESIAN_POINT ( 'NONE',  ( 1.014069264286642014, 0.4235180831842794702, 1.062992125984251635 ) ) ;
#39061=EDGE_CURVE ( 'NONE', #20081, #13474, #39409, .T. ) ;
#39076=LINE ( 'NONE', #7083, #32479 ) ;
#39159=DIRECTION ( 'NONE',  ( 0.000000000000000000, 1.000000000000000000, 0.000000000000000000 ) ) ;
#39163=AXIS2_PLACEMENT_3D ( 'NONE', #23213, #35356, #30718 ) ;
#39194=LINE ( 'NONE', #46905, #43787 ) ;
#39199=DIRECTION ( 'NONE',  ( -0.7071067811865466846, 0.000000000000000000, 0.7071067811865483499 ) ) ;
#39202=FACE_OUTER_BOUND ( 'NONE', #50200, .T. ) ;
#39221=ORIENTED_EDGE ( 'NONE', *, *, #31887, .F. ) ;
#39222=EDGE_CURVE ( 'NONE', #50189, #7253, #13834, .T. ) ;
#39291=VERTEX_POINT ( 'NONE', #17449 ) ;
#39316=AXIS2_PLACEMENT_3D ( 'NONE', #24607, #40610, #49066 ) ;
#39394=ORIENTED_EDGE ( 'NONE', *, *, #23973, .T. ) ;
#39409=LINE ( 'NONE', #20295, #27316 ) ;
#39412=ADVANCED_FACE ( 'NONE', ( #30597 ), #15097, .T. ) ;
#39538=EDGE_CURVE ( 'NONE', #5108, #4189, #4491, .T. ) ;
#39613=DIRECTION ( 'NONE',  ( 0.000000000000000000, -1.000000000000000000, 0.000000000000000000 ) ) ;
#39634=CARTESIAN_POINT ( 'NONE',  ( 1.062992125984252079, 0.5905511811023621549, 1.014069264286641792 ) ) ;
#39647=VECTOR ( 'NONE', #10538, 39.37007874015748143 ) ;
#39776=ORIENTED_EDGE ( 'NONE', *, *, #16701, .F. ) ;
#39814=ORIENTED_EDGE ( 'NONE', *, *, #28818, .F. ) ;
#39841=EDGE_CURVE ( 'NONE', #45101, #26202, #7036, .T. ) ;
#39918=LINE ( 'NONE', #1189, #44332 ) ;
#39931=CARTESIAN_POINT ( 'NONE',  ( -1.122047244094487750, 0.5314960629921255952, 1.062992125984251413 ) ) ;
#39981=VECTOR ( 'NONE', #46801, 39.37007874015748143 ) ;
#40015=FACE_OUTER_BOUND ( 'NONE', #15456, .T. ) ;
#40023=ADVANCED_FACE ( 'NONE', ( #49759 ), #31204, .F. ) ;
#40035=ORIENTED_EDGE ( 'NONE', *, *, #7, .T. ) ;
#40047=DIRECTION ( 'NONE',  ( 0.000000000000000000, -1.000000000000000000, 0.000000000000000000 ) ) ;
#40137=CARTESIAN_POINT ( 'NONE',  ( -1.181102362204724310, 0.000000000000000000, -1.062992125984252079 ) ) ;
#40159=CARTESIAN_POINT ( 'NONE',  ( 0.000000000000000000, 0.5070346321433212289, -0.9794755770252108196 ) ) ;
#40165=CARTESIAN_POINT ( 'NONE',  ( 1.062992125984252079, 0.4235180831842795257, -6.146657985744593474E-17 ) ) ;
#40192=FACE_OUTER_BOUND ( 'NONE', #19288, .T. ) ;
#40201=EDGE_CURVE ( 'NONE', #2075, #33385, #8219, .T. ) ;
#40296=ADVANCED_FACE ( 'NONE', ( #31716 ), #15705, .F. ) ;
#40357=DIRECTION ( 'NONE',  ( 0.000000000000000000, 0.000000000000000000, 1.000000000000000000 ) ) ;
#40388=VECTOR ( 'NONE', #513, 39.37007874015748143 ) ;
#40459=ORIENTED_EDGE ( 'NONE', *, *, #35471, .T. ) ;
#40462=DIRECTION ( 'NONE',  ( -0.5773502691896253980, 0.5773502691896246208, 0.5773502691896272854 ) ) ;
#40546=EDGE_CURVE ( 'NONE', #32429, #47028, #49449, .T. ) ;
#40593=DIRECTION ( 'NONE',  ( 0.000000000000000000, -1.000000000000000000, 0.000000000000000000 ) ) ;
#40610=DIRECTION ( 'NONE',  ( 0.5773502691896245098, 0.5773502691896259531, -0.5773502691896270633 ) ) ;
#40763=ORIENTED_EDGE ( 'NONE', *, *, #29604, .T. ) ;
#40797=DIRECTION ( 'NONE',  ( -0.7071067811865481278, 0.7071067811865469066, -1.221861889385012670E-15 ) ) ;
#40890=DIRECTION ( 'NONE',  ( 5.782411586589357392E-17, 0.000000000000000000, 1.000000000000000000 ) ) ;
#40900=DIRECTION ( 'NONE',  ( 0.7071067811865463515, 0.000000000000000000, -0.7071067811865487940 ) ) ;
#41019=CARTESIAN_POINT ( 'NONE',  ( -1.014069264286641792, 0.4724409448818898127, -1.014069264286642458 ) ) ;
#41073=LENGTH_MEASURE_WITH_UNIT ( LENGTH_MEASURE( 0.02539999999999999897 ), #48508 );
#41176=VECTOR ( 'NONE', #36741, 39.37007874015748143 ) ;
#41217=MANIFOLD_SOLID_BREP ( 'Shell1', #33708 ) ;
#41373=CARTESIAN_POINT ( 'NONE',  ( -1.181102362204724310, 0.000000000000000000, -1.181102362204724754 ) ) ;
#41388=DIRECTION ( 'NONE',  ( 1.000000000000000000, 0.000000000000000000, 0.000000000000000000 ) ) ;
#41429=CARTESIAN_POINT ( 'NONE',  ( -1.025452293874513199, 0.4479795140330847802, -1.038530695135447157 ) ) ;
#41442=ORIENTED_EDGE ( 'NONE', *, *, #4473, .F. ) ;
#41512=LINE ( 'NONE', #6404, #30110 ) ;
#41603=AXIS2_PLACEMENT_3D ( 'NONE', #50398, #50644, #15342 ) ;
#41629=ORIENTED_EDGE ( 'NONE', *, *, #47296, .T. ) ;
#41692=VECTOR ( 'NONE', #14571, 39.37007874015748854 ) ;
#41949=EDGE_CURVE ( 'NONE', #10297, #50880, #39918, .T. ) ;
#41982=VERTEX_POINT ( 'NONE', #8169 ) ;
#42020=DIRECTION ( 'NONE',  ( -0.5773502691896266192, 0.5773502691896260641, -0.5773502691896246208 ) ) ;
#42067=EDGE_LOOP ( 'NONE', ( #33507, #42401, #17043, #12174 ) ) ;
#42098=DIRECTION ( 'NONE',  ( 0.000000000000000000, -1.000000000000000000, 0.000000000000000000 ) ) ;
#42125=LINE ( 'NONE', #41373, #11526 ) ;
#42136=LINE ( 'NONE', #42640, #46806 ) ;
#42159=DIRECTION ( 'NONE',  ( -1.000000000000000000, 0.000000000000000000, 0.000000000000000000 ) ) ;
#42181=LINE ( 'NONE', #49386, #19149 ) ;
#42225=CARTESIAN_POINT ( 'NONE',  ( 1.062992125984251635, 0.4724409448818890911, 1.181102362204724088 ) ) ;
#42394=LINE ( 'NONE', #18666, #20538 ) ;
#42401=ORIENTED_EDGE ( 'NONE', *, *, #4287, .T. ) ;
#42536=LINE ( 'NONE', #7176, #4492 ) ;
#42546=VERTEX_POINT ( 'NONE', #39026 ) ;
#42552=ORIENTED_EDGE ( 'NONE', *, *, #38554, .T. ) ;
#42640=CARTESIAN_POINT ( 'NONE',  ( 0.7317238754971220338, 0.1411726943947593793, 1.345337514773770948 ) ) ;
#42643=DIRECTION ( 'NONE',  ( 1.000000000000000000, -0.000000000000000000, 0.000000000000000000 ) ) ;
#42644=EDGE_CURVE ( 'NONE', #23981, #17210, #42136, .T. ) ;
#42695=ADVANCED_FACE ( 'NONE', ( #19893 ), #35413, .F. ) ;
#42835=FACE_OUTER_BOUND ( 'NONE', #8011, .T. ) ;
#42916=AXIS2_PLACEMENT_3D ( 'NONE', #27493, #15125, #30877 ) ;
#42942=DIRECTION ( 'NONE',  ( -0.000000000000000000, -1.000000000000000000, 0.000000000000000000 ) ) ;
#42988=DIRECTION ( 'NONE',  ( 0.5773502691896261751, 0.5773502691896261751, 0.5773502691896248429 ) ) ;
#43010=DIRECTION ( 'NONE',  ( 0.000000000000000000, -1.000000000000000000, -0.000000000000000000 ) ) ;
#43011=VECTOR ( 'NONE', #40797, 39.37007874015748143 ) ;
#43020=VECTOR ( 'NONE', #46095, 39.37007874015748854 ) ;
#43040=ORIENTED_EDGE ( 'NONE', *, *, #40201, .F. ) ;
#43045=VERTEX_POINT ( 'NONE', #34786 ) ;
#43056=DIRECTION ( 'NONE',  ( 0.000000000000000000, -1.000000000000000000, 0.000000000000000000 ) ) ;
#43073=FACE_OUTER_BOUND ( 'NONE', #28024, .T. ) ;
#43077=LINE ( 'NONE', #27848, #50575 ) ;
#43107=EDGE_CURVE ( 'NONE', #33385, #30631, #11788, .T. ) ;
#43149=ORIENTED_EDGE ( 'NONE', *, *, #33657, .F. ) ;
#43160=ORIENTED_EDGE ( 'NONE', *, *, #26070, .T. ) ;
#43208=ADVANCED_FACE ( 'NONE', ( #40192 ), #29064, .F. ) ;
#43218=ORIENTED_EDGE ( 'NONE', *, *, #17846, .T. ) ;
#43289=ORIENTED_EDGE ( 'NONE', *, *, #854, .F. ) ;
#43353=VECTOR ( 'NONE', #32525, 39.37007874015748143 ) ;
#43562=DIRECTION ( 'NONE',  ( -0.7071067811865466846, 0.000000000000000000, 0.7071067811865483499 ) ) ;
#43669=EDGE_LOOP ( 'NONE', ( #46695, #24283, #34892 ) ) ;
#43691=CARTESIAN_POINT ( 'NONE',  ( -1.181102362204724310, 0.5905511811023621549, -1.181102362204724754 ) ) ;
#43696=ORIENTED_EDGE ( 'NONE', *, *, #47296, .F. ) ;
#43764=FACE_OUTER_BOUND ( 'NONE', #27801, .T. ) ;
#43787=VECTOR ( 'NONE', #11577, 39.37007874015748143 ) ;
#43831=EDGE_CURVE ( 'NONE', #35502, #5108, #42394, .T. ) ;
#43933=LINE ( 'NONE', #8580, #5420 ) ;
#43996=AXIS2_PLACEMENT_3D ( 'NONE', #7032, #45992, #22524 ) ;
#44326=CARTESIAN_POINT ( 'NONE',  ( -1.062992125984251413, 0.5905511811023621549, 1.062992125984251413 ) ) ;
#44332=VECTOR ( 'NONE', #676, 39.37007874015748143 ) ;
#44432=( GEOMETRIC_REPRESENTATION_CONTEXT ( 3 ) GLOBAL_UNCERTAINTY_ASSIGNED_CONTEXT ( ( #922 ) ) GLOBAL_UNIT_ASSIGNED_CONTEXT ( ( #37201, #22460, #29699 ) ) REPRESENTATION_CONTEXT ( 'NONE', 'WORKASPACE' ) );
#44448=ORIENTED_EDGE ( 'NONE', *, *, #24053, .T. ) ;
#44486=EDGE_CURVE ( 'NONE', #4657, #30221, #32077, .T. ) ;
#44601=DIRECTION ( 'NONE',  ( 0.5773502691896256200, 0.5773502691896271743, -0.5773502691896242878 ) ) ;
#44630=ORIENTED_EDGE ( 'NONE', *, *, #23973, .F. ) ;
#44631=ORIENTED_EDGE ( 'NONE', *, *, #46300, .T. ) ;
#44731=CARTESIAN_POINT ( 'NONE',  ( 0.000000000000000000, 0.5905511811023621549, -1.062992125984252079 ) ) ;
#44757=ORIENTED_EDGE ( 'NONE', *, *, #28998, .T. ) ;
#44764=EDGE_LOOP ( 'NONE', ( #28726, #48455, #692, #24336 ) ) ;
#44806=DIRECTION ( 'NONE',  ( 0.7071067811865466846, 0.000000000000000000, 0.7071067811865483499 ) ) ;
#44973=AXIS2_PLACEMENT_3D ( 'NONE', #7457, #3584, #19317 ) ;
#45028=ORIENTED_EDGE ( 'NONE', *, *, #33029, .T. ) ;
#45032=EDGE_LOOP ( 'NONE', ( #36040, #49874, #13985, #39221 ) ) ;
#45067=DIRECTION ( 'NONE',  ( 0.000000000000000000, 1.000000000000000000, 0.000000000000000000 ) ) ;
#45069=CARTESIAN_POINT ( 'NONE',  ( -1.062992125984251413, 0.5314960629921257063, -1.122047244094488416 ) ) ;
#45101=VERTEX_POINT ( 'NONE', #9279 ) ;
#45215=CARTESIAN_POINT ( 'NONE',  ( -1.181102362204724088, 0.4724409448818890911, 1.181102362204724088 ) ) ;
#45346=DIRECTION ( 'NONE',  ( -0.7071067811865466846, -0.7071067811865483499, 7.903458058585701571E-16 ) ) ;
#45549=CARTESIAN_POINT ( 'NONE',  ( -0.9794755770252101534, 0.000000000000000000, 1.097585813245683051 ) ) ;
#45568=LINE ( 'NONE', #45069, #23501 ) ;
#45639=AXIS2_PLACEMENT_3D ( 'NONE', #47237, #28415, #40047 ) ;
#45664=PRODUCT_DEFINITION_FORMATION_WITH_SPECIFIED_SOURCE ( 'ANY', '', #8350, .NOT_KNOWN. ) ;
#45705=AXIS2_PLACEMENT_3D ( 'NONE', #47896, #15926, #20830 ) ;
#45738=VECTOR ( 'NONE', #48149, 39.37007874015748143 ) ;
#45779=ADVANCED_FACE ( 'NONE', ( #50188 ), #19239, .F. ) ;
#45797=LINE ( 'NONE', #10460, #9127 ) ;
#45826=VECTOR ( 'NONE', #6625, 39.37007874015747433 ) ;
#45938=EDGE_CURVE ( 'NONE', #14593, #48594, #16141, .T. ) ;
#45992=DIRECTION ( 'NONE',  ( 0.000000000000000000, 0.7071067811865466846, 0.7071067811865483499 ) ) ;
#46015=CARTESIAN_POINT ( 'NONE',  ( 0.000000000000000000, 0.4724409448818898127, -1.014069264286642236 ) ) ;
#46095=DIRECTION ( 'NONE',  ( 0.7071067811865486830, 2.775557561562891351E-17, 0.7071067811865462405 ) ) ;
#46098=VECTOR ( 'NONE', #36285, 39.37007874015748143 ) ;
#46099=ORIENTED_EDGE ( 'NONE', *, *, #35919, .F. ) ;
#46227=ADVANCED_FACE ( 'NONE', ( #40015 ), #4138, .T. ) ;
#46235=CARTESIAN_POINT ( 'NONE',  ( -1.062992125984252079, 0.000000000000000000, -1.181102362204724754 ) ) ;
#46291=EDGE_CURVE ( 'NONE', #30940, #31066, #3627, .T. ) ;
#46300=EDGE_CURVE ( 'NONE', #17210, #39291, #29419, .T. ) ;
#46311=CARTESIAN_POINT ( 'NONE',  ( 0.000000000000000000, 0.5905511811023621549, 1.062992125984251413 ) ) ;
#46378=PLANE ( 'NONE',  #11056 ) ;
#46491=CARTESIAN_POINT ( 'NONE',  ( -1.181102362204724088, 0.000000000000000000, 1.062992125984251635 ) ) ;
#46518=CARTESIAN_POINT ( 'NONE',  ( -1.062992125984250968, 0.4724409448818890911, 1.181102362204724088 ) ) ;
#46558=DIRECTION ( 'NONE',  ( 0.000000000000000000, 0.7071067811865466846, 0.7071067811865483499 ) ) ;
#46565=CARTESIAN_POINT ( 'NONE',  ( 1.181102362204724532, 0.000000000000000000, 1.062992125984251413 ) ) ;
#46678=PLANE ( 'NONE',  #39163 ) ;
#46695=ORIENTED_EDGE ( 'NONE', *, *, #6385, .F. ) ;
#46736=DIRECTION ( 'NONE',  ( -0.7071067811865466846, -0.000000000000000000, -0.7071067811865483499 ) ) ;
#46801=DIRECTION ( 'NONE',  ( -1.156482317317871478E-16, 0.000000000000000000, -1.000000000000000000 ) ) ;
#46806=VECTOR ( 'NONE', #26393, 39.37007874015748854 ) ;
#46850=ORIENTED_EDGE ( 'NONE', *, *, #38272, .F. ) ;
#46905=CARTESIAN_POINT ( 'NONE',  ( -0.9794755770252102645, 0.5070346321433213399, -1.025452293874513643 ) ) ;
#46906=CARTESIAN_POINT ( 'NONE',  ( 0.9948011493083114276, 0.4042499682059490507, -1.112911385528784658 ) ) ;
#46921=EDGE_CURVE ( 'NONE', #30631, #48480, #33762, .T. ) ;
#46951=DIRECTION ( 'NONE',  ( -0.7071067811865483499, -0.000000000000000000, 0.7071067811865466846 ) ) ;
#46961=SHAPE_REPRESENTATION_RELATIONSHIP ( 'NONE' , 'NONE' ,  #5020, #37253 ) ;
#46973=CARTESIAN_POINT ( 'NONE',  ( -1.025452293874513199, 0.4610579152940180170, 1.025452293874513199 ) ) ;
#47014=EDGE_CURVE ( 'NONE', #7604, #47727, #4273, .T. ) ;
#47028=VERTEX_POINT ( 'NONE', #3258 ) ;
#47053=CARTESIAN_POINT ( 'NONE',  ( -1.181102362204724310, 0.4724409448818890911, -1.181102362204724754 ) ) ;
#47122=ORIENTED_EDGE ( 'NONE', *, *, #22379, .T. ) ;
#47172=EDGE_CURVE ( 'NONE', #5108, #12139, #48367, .T. ) ;
#47190=EDGE_LOOP ( 'NONE', ( #9493, #34268, #11325, #2222 ) ) ;
#47206=CARTESIAN_POINT ( 'NONE',  ( 1.062992125984252079, 0.000000000000000000, -1.181102362204724754 ) ) ;
#47223=AXIS2_PLACEMENT_3D ( 'NONE', #11107, #22727, #40890 ) ;
#47237=CARTESIAN_POINT ( 'NONE',  ( -0.9794755770252101534, 0.5905511811023621549, 1.097585813245683051 ) ) ;
#47296=EDGE_CURVE ( 'NONE', #23981, #22477, #42181, .T. ) ;
#47341=VECTOR ( 'NONE', #42942, 39.37007874015748143 ) ;
#47355=CARTESIAN_POINT ( 'NONE',  ( 0.000000000000000000, 0.5905511811023621549, 0.000000000000000000 ) ) ;
#47446=AXIS2_PLACEMENT_3D ( 'NONE', #21121, #26006, #5367 ) ;
#47491=VECTOR ( 'NONE', #31650, 39.37007874015748143 ) ;
#47523=LINE ( 'NONE', #16847, #16543 ) ;
#47562=EDGE_CURVE ( 'NONE', #14593, #7604, #24854, .T. ) ;
#47568=ORIENTED_EDGE ( 'NONE', *, *, #11208, .T. ) ;
#47712=ORIENTED_EDGE ( 'NONE', *, *, #38554, .F. ) ;
#47727=VERTEX_POINT ( 'NONE', #22257 ) ;
#47817=CARTESIAN_POINT ( 'NONE',  ( 0.9794755770252105975, 0.5070346321433210068, 1.025452293874513199 ) ) ;
#47851=CARTESIAN_POINT ( 'NONE',  ( -1.062992125984251413, 0.5905511811023621549, 1.181102362204724088 ) ) ;
#47866=ORIENTED_EDGE ( 'NONE', *, *, #14896, .F. ) ;
#47878=DIRECTION ( 'NONE',  ( -0.7071067811865483499, -2.200518442539857142E-16, 0.7071067811865465735 ) ) ;
#47880=CARTESIAN_POINT ( 'NONE',  ( -1.181102362204724310, 0.5905511811023621549, -1.062992125984252079 ) ) ;
#47893=AXIS2_PLACEMENT_3D ( 'NONE', #46311, #46558, #11225 ) ;
#47896=CARTESIAN_POINT ( 'NONE',  ( -0.9794755770252102645, 0.5070346321433212289, 1.132746185074374460E-16 ) ) ;
#47913=CARTESIAN_POINT ( 'NONE',  ( 0.9794755770252103755, 0.4349011127721511549, -1.097585813245683495 ) ) ;
#48003=DIRECTION ( 'NONE',  ( -0.000000000000000000, 1.000000000000000000, 0.000000000000000000 ) ) ;
#48032=ORIENTED_EDGE ( 'NONE', *, *, #5898, .T. ) ;
#48099=ORIENTED_EDGE ( 'NONE', *, *, #1076, .F. ) ;
#48149=DIRECTION ( 'NONE',  ( -0.7071067811865466846, -0.7071067811865483499, 7.903458058585701571E-16 ) ) ;
#48260=CARTESIAN_POINT ( 'NONE',  ( 1.062992125984251413, 0.5905511811023621549, 1.062992125984251413 ) ) ;
#48357=DIRECTION ( 'NONE',  ( -0.5773502691896261751, 0.5773502691896261751, 0.5773502691896248429 ) ) ;
#48367=LINE ( 'NONE', #40165, #8441 ) ;
#48396=CARTESIAN_POINT ( 'NONE',  ( 1.014069264286642014, 0.5905511811023621549, 1.062992125984251635 ) ) ;
#48419=AXIS2_PLACEMENT_3D ( 'NONE', #46906, #27311, #14446 ) ;
#48455=ORIENTED_EDGE ( 'NONE', *, *, #4287, .F. ) ;
#48480=VERTEX_POINT ( 'NONE', #46518 ) ;
#48508=( LENGTH_UNIT ( ) NAMED_UNIT ( * ) SI_UNIT ( $, .METRE. ) );
#48567=FACE_OUTER_BOUND ( 'NONE', #34180, .T. ) ;
#48591=ORIENTED_EDGE ( 'NONE', *, *, #46291, .T. ) ;
#48594=VERTEX_POINT ( 'NONE', #18425 ) ;
#48610=VECTOR ( 'NONE', #35682, 39.37007874015748854 ) ;
#48736=ORIENTED_EDGE ( 'NONE', *, *, #7, .F. ) ;
#48813=LINE ( 'NONE', #45215, #3864 ) ;
#48830=FACE_OUTER_BOUND ( 'NONE', #47190, .T. ) ;
#48943=ADVANCED_FACE ( 'NONE', ( #23180 ), #35572, .T. ) ;
#48950=ORIENTED_EDGE ( 'NONE', *, *, #21245, .F. ) ;
#49022=FACE_OUTER_BOUND ( 'NONE', #42067, .T. ) ;
#49043=VERTEX_POINT ( 'NONE', #44326 ) ;
#49066=DIRECTION ( 'NONE',  ( 0.000000000000000000, 0.7071067811865482389, 0.7071067811865467956 ) ) ;
#49223=ORIENTED_EDGE ( 'NONE', *, *, #39222, .F. ) ;
#49230=CARTESIAN_POINT ( 'NONE',  ( 0.000000000000000000, 0.000000000000000000, 0.000000000000000000 ) ) ;
#49252=ORIENTED_EDGE ( 'NONE', *, *, #42644, .F. ) ;
#49294=AXIS2_PLACEMENT_3D ( 'NONE', #25423, #43562, #8215 ) ;
#49382=VECTOR ( 'NONE', #21522, 39.37007874015748143 ) ;
#49386=CARTESIAN_POINT ( 'NONE',  ( 0.000000000000000000, 0.4235180831842794702, 1.062992125984251635 ) ) ;
#49434=ORIENTED_EDGE ( 'NONE', *, *, #36855, .F. ) ;
#49449=LINE ( 'NONE', #14386, #11421 ) ;
#49504=ORIENTED_EDGE ( 'NONE', *, *, #24053, .F. ) ;
#49526=ADVANCED_FACE ( 'NONE', ( #131 ), #15881, .F. ) ;
#49560=ORIENTED_EDGE ( 'NONE', *, *, #13164, .T. ) ;
#49591=PLANE ( 'NONE',  #43996 ) ;
#49648=DIRECTION ( 'NONE',  ( -0.7071067811865483499, -1.442222014787672788E-15, -0.7071067811865465735 ) ) ;
#49759=FACE_OUTER_BOUND ( 'NONE', #43669, .T. ) ;
#49816=CARTESIAN_POINT ( 'NONE',  ( -1.014069264286641570, 0.000000000000000000, 1.062992125984251635 ) ) ;
#49874=ORIENTED_EDGE ( 'NONE', *, *, #11572, .F. ) ;
#49881=LINE ( 'NONE', #41429, #41692 ) ;
#49885=DIRECTION ( 'NONE',  ( -1.000000000000000000, 0.000000000000000000, 0.000000000000000000 ) ) ;
#49943=ORIENTED_EDGE ( 'NONE', *, *, #15259, .F. ) ;
#49963=CARTESIAN_POINT ( 'NONE',  ( 1.025452293874513421, 0.4610579152940179615, -1.025452293874514087 ) ) ;
#49970=CARTESIAN_POINT ( 'NONE',  ( -1.046684505418381761, 0.4561333243160194950, 1.030376884852511665 ) ) ;
#50095=FACE_OUTER_BOUND ( 'NONE', #23785, .T. ) ;
#50128=DIRECTION ( 'NONE',  ( 0.7071067811865469066, 0.7071067811865481278, -4.088782444488994004E-17 ) ) ;
#50187=CARTESIAN_POINT ( 'NONE',  ( -1.345337514773770282, 0.1411726943947604063, 0.7317238754971241432 ) ) ;
#50188=FACE_OUTER_BOUND ( 'NONE', #19627, .T. ) ;
#50189=VERTEX_POINT ( 'NONE', #49816 ) ;
#50200=EDGE_LOOP ( 'NONE', ( #50801, #7123, #37729 ) ) ;
#50205=DIRECTION ( 'NONE',  ( 1.156482317317871478E-16, -0.000000000000000000, 1.000000000000000000 ) ) ;
#50226=VERTEX_POINT ( 'NONE', #8522 ) ;
#50398=CARTESIAN_POINT ( 'NONE',  ( -1.062992125984251413, 0.5905511811023621549, 1.229331597148917955E-16 ) ) ;
#50575=VECTOR ( 'NONE', #3860, 39.37007874015748143 ) ;
#50602=AXIS2_PLACEMENT_3D ( 'NONE', #24711, #40462, #5081 ) ;
#50644=DIRECTION ( 'NONE',  ( -0.7071067811865483499, 0.7071067811865466846, 8.177564888978005264E-17 ) ) ;
#50801=ORIENTED_EDGE ( 'NONE', *, *, #40546, .F. ) ;
#50805=CARTESIAN_POINT ( 'NONE',  ( 1.181102362204724532, 0.000000000000000000, 1.062992125984251413 ) ) ;
#50810=VECTOR ( 'NONE', #31358, 39.37007874015748143 ) ;
#50817=( CONVERSION_BASED_UNIT ( 'INCH', #19125 ) LENGTH_UNIT ( ) NAMED_UNIT ( #20876 ) );
#50825=ORIENTED_EDGE ( 'NONE', *, *, #20910, .T. ) ;
#50880=VERTEX_POINT ( 'NONE', #10704 ) ;
#50916=EDGE_CURVE ( 'NONE', #20081, #26402, #39076, .T. ) ;
#50946=ORIENTED_EDGE ( 'NONE', *, *, #39538, .T. ) ;
#50958=CARTESIAN_POINT ( 'NONE',  ( -1.014069264286641570, 0.4724409448818898127, 1.172753172683044372E-16 ) ) ;
#51003=ORIENTED_EDGE ( 'NONE', *, *, #47014, .F. ) ;
#51007=ADVANCED_FACE ( 'NONE', ( #4980 ), #31848, .F. ) ;
#51016=ORIENTED_EDGE ( 'NONE', *, *, #1076, .T. ) ;
#51067=COLOUR_RGB('Light Blue',0.38,0.62,0.78);
#51068=FILL_AREA_STYLE_COLOUR('',#51067);
#51069=FILL_AREA_STYLE('',(#51068));
#51070=SURFACE_STYLE_FILL_AREA(#51069);
#51071=SURFACE_SIDE_STYLE('',(#51070));
#51072=SURFACE_STYLE_USAGE(.BOTH.,#51071);
#51073=PRESENTATION_STYLE_ASSIGNMENT((#51072));
ENDSEC;
END-ISO-10303-21;
